ISO-10303-21;
HEADER;
/* Generated by software containing ST-Developer
 * from STEP Tools, Inc. (www.steptools.com) 
 */

FILE_DESCRIPTION(
/* description */ (''),
/* implementation_level */ '2;1');

FILE_NAME(
/* name */ 'Front_Block.step',
/* time_stamp */ '2026-10-19T01:30:23+06:00',
/* author */ (''),
/* organization */ (''),
/* preprocessor_version */ 'ST-DEVELOPER v20.2',
/* originating_system */ 'Autodesk Translation Framework v15.15.0.0',
/* authorisation */ '');

FILE_SCHEMA (('AUTOMOTIVE_DESIGN { 1 0 10303 214 3 1 1 }'));
ENDSEC;

DATA;
#10=MECHANICAL_DESIGN_GEOMETRIC_PRESENTATION_REPRESENTATION('',(#96),#10639);
#59=B_SPLINE_CURVE_WITH_KNOTS('',3,(#10339,#10340,#10341,#10342,#10343,
#10344,#10345,#10346,#10347,#10348,#10349,#10350,#10351,#10352),
 .UNSPECIFIED.,.F.,.F.,(4,2,2,2,2,2,4),(-0.0546723895048706,-0.0456918425711812,
-0.0355825901397237,-0.0226053755936092,-0.0114630731161328,0.,0.000317608874346033),
 .UNSPECIFIED.);
#60=B_SPLINE_CURVE_WITH_KNOTS('',3,(#10371,#10372,#10373,#10374,#10375,
#10376,#10377,#10378,#10379,#10380,#10381,#10382,#10383,#10384),
 .UNSPECIFIED.,.F.,.F.,(4,2,2,2,2,2,4),(-0.0545709206888463,-0.0542557323018554,
-0.0428800190516867,-0.0318226318386046,-0.0189443163854003,-0.00891210636484469,
0.),.UNSPECIFIED.);
#61=B_SPLINE_CURVE_WITH_KNOTS('',3,(#10390,#10391,#10392,#10393,#10394,
#10395,#10396,#10397,#10398,#10399,#10400,#10401,#10402,#10403),
 .UNSPECIFIED.,.F.,.F.,(4,2,2,2,2,2,4),(-0.054570920688858,-0.0542557323018634,
-0.0428800190517046,-0.0318226318386095,-0.0189443163853947,-0.00891210636484256,
0.),.UNSPECIFIED.);
#62=B_SPLINE_CURVE_WITH_KNOTS('',3,(#10409,#10410,#10411,#10412,#10413,
#10414,#10415,#10416,#10417,#10418,#10419,#10420,#10421,#10422),
 .UNSPECIFIED.,.F.,.F.,(4,2,2,2,2,2,4),(-0.0546723899568943,-0.0456918429465685,
-0.035582590428848,-0.0226053757720057,-0.0114630731991726,0.,0.000317608880617367),
 .UNSPECIFIED.);
#63=B_SPLINE_CURVE_WITH_KNOTS('',3,(#10459,#10460,#10461,#10462,#10463,
#10464,#10465,#10466,#10467,#10468,#10469,#10470,#10471,#10472),
 .UNSPECIFIED.,.F.,.F.,(4,2,2,2,2,2,4),(-0.0545709206888251,-0.0542557323018344,
-0.0428800190516725,-0.031822631838589,-0.0189443163853906,-0.00891210636484253,
0.),.UNSPECIFIED.);
#64=B_SPLINE_CURVE_WITH_KNOTS('',3,(#10484,#10485,#10486,#10487,#10488,
#10489,#10490,#10491,#10492,#10493,#10494,#10495,#10496,#10497),
 .UNSPECIFIED.,.F.,.F.,(4,2,2,2,2,2,4),(-0.0546723899569042,-0.0456918429465809,
-0.0355825904288576,-0.0226053757720114,-0.0114630731991751,0.,0.000317608880617457),
 .UNSPECIFIED.);
#65=B_SPLINE_CURVE_WITH_KNOTS('',3,(#10506,#10507,#10508,#10509,#10510,
#10511,#10512,#10513,#10514,#10515,#10516,#10517,#10518,#10519),
 .UNSPECIFIED.,.F.,.F.,(4,2,2,2,2,2,4),(-0.0546723899569031,-0.0456918429465823,
-0.0355825904288603,-0.0226053757720111,-0.0114630731991739,0.,0.000317608880617373),
 .UNSPECIFIED.);
#66=B_SPLINE_CURVE_WITH_KNOTS('',3,(#10528,#10529,#10530,#10531,#10532,
#10533,#10534,#10535,#10536,#10537,#10538,#10539,#10540,#10541),
 .UNSPECIFIED.,.F.,.F.,(4,2,2,2,2,2,4),(-0.0545709206996626,-0.0542557323162056,
-0.0428800190513851,-0.0318226318385961,-0.0189443163854002,-0.00891210636484565,
0.),.UNSPECIFIED.);
#76=SHAPE_REPRESENTATION_RELATIONSHIP('SRR','None',#10686,#86);
#86=ADVANCED_BREP_SHAPE_REPRESENTATION('',(#106),#10638);
#96=STYLED_ITEM('',(#10769),#106);
#106=MANIFOLD_SOLID_BREP('Front_Block',#5722);
#143=SPHERICAL_SURFACE('',#6518,0.3);
#144=SPHERICAL_SURFACE('',#6522,0.299999999999994);
#145=SPHERICAL_SURFACE('',#6526,0.300000000000011);
#146=SPHERICAL_SURFACE('',#6531,0.299999999999998);
#147=SPHERICAL_SURFACE('',#6536,0.3);
#148=SPHERICAL_SURFACE('',#6542,0.299999999999994);
#149=SPHERICAL_SURFACE('',#6547,0.3);
#150=SPHERICAL_SURFACE('',#6556,0.3);
#151=SPHERICAL_SURFACE('',#6571,0.299999999999998);
#152=SPHERICAL_SURFACE('',#6581,0.299999999999994);
#153=SPHERICAL_SURFACE('',#6586,0.299999999999994);
#154=SPHERICAL_SURFACE('',#6591,0.3);
#155=SPHERICAL_SURFACE('',#6596,0.299999999999994);
#156=SPHERICAL_SURFACE('',#6602,0.299999999999998);
#157=SPHERICAL_SURFACE('',#6606,0.300000000000002);
#158=SPHERICAL_SURFACE('',#6611,0.3);
#159=SPHERICAL_SURFACE('',#6620,0.3);
#160=SPHERICAL_SURFACE('',#6624,0.3);
#161=SPHERICAL_SURFACE('',#6628,0.3);
#162=SPHERICAL_SURFACE('',#6633,0.299999999999994);
#235=TOROIDAL_SURFACE('',#6490,2.29999999999999,0.3);
#236=TOROIDAL_SURFACE('',#6498,2.29999999999999,0.3);
#237=TOROIDAL_SURFACE('',#6503,2.29999999999999,0.3);
#238=TOROIDAL_SURFACE('',#6512,2.29999999999999,0.3);
#239=TOROIDAL_SURFACE('',#6551,0.600000000000001,0.3);
#240=TOROIDAL_SURFACE('',#6561,0.600000000000001,0.299999999999994);
#241=TOROIDAL_SURFACE('',#6566,0.600000000000001,0.299999999999976);
#242=TOROIDAL_SURFACE('',#6576,0.600000000000001,0.3);
#243=TOROIDAL_SURFACE('',#6643,4.3,0.3);
#244=TOROIDAL_SURFACE('',#6647,4.3,0.3);
#245=TOROIDAL_SURFACE('',#6650,4.3,0.3);
#246=TOROIDAL_SURFACE('',#6653,4.3,0.3);
#286=FACE_BOUND('',#1104,.T.);
#287=FACE_BOUND('',#1105,.T.);
#288=FACE_BOUND('',#1111,.T.);
#289=FACE_BOUND('',#1112,.T.);
#290=FACE_BOUND('',#1189,.T.);
#291=FACE_BOUND('',#1190,.T.);
#292=FACE_BOUND('',#1191,.T.);
#293=FACE_BOUND('',#1192,.T.);
#367=PLANE('',#6494);
#368=PLANE('',#6508);
#369=PLANE('',#6670);
#370=PLANE('',#6673);
#371=PLANE('',#6674);
#372=PLANE('',#6675);
#373=PLANE('',#6676);
#374=PLANE('',#6677);
#375=PLANE('',#6678);
#376=PLANE('',#6679);
#377=PLANE('',#6680);
#378=PLANE('',#6681);
#379=PLANE('',#6682);
#380=PLANE('',#6683);
#381=PLANE('',#6684);
#382=PLANE('',#6685);
#676=FACE_OUTER_BOUND('',#1102,.T.);
#677=FACE_OUTER_BOUND('',#1103,.T.);
#678=FACE_OUTER_BOUND('',#1106,.T.);
#679=FACE_OUTER_BOUND('',#1107,.T.);
#680=FACE_OUTER_BOUND('',#1108,.T.);
#681=FACE_OUTER_BOUND('',#1109,.T.);
#682=FACE_OUTER_BOUND('',#1110,.T.);
#683=FACE_OUTER_BOUND('',#1113,.T.);
#684=FACE_OUTER_BOUND('',#1114,.T.);
#685=FACE_OUTER_BOUND('',#1115,.T.);
#686=FACE_OUTER_BOUND('',#1116,.T.);
#687=FACE_OUTER_BOUND('',#1117,.T.);
#688=FACE_OUTER_BOUND('',#1118,.T.);
#689=FACE_OUTER_BOUND('',#1119,.T.);
#690=FACE_OUTER_BOUND('',#1120,.T.);
#691=FACE_OUTER_BOUND('',#1121,.T.);
#692=FACE_OUTER_BOUND('',#1122,.T.);
#693=FACE_OUTER_BOUND('',#1123,.T.);
#694=FACE_OUTER_BOUND('',#1124,.T.);
#695=FACE_OUTER_BOUND('',#1125,.T.);
#696=FACE_OUTER_BOUND('',#1126,.T.);
#697=FACE_OUTER_BOUND('',#1127,.T.);
#698=FACE_OUTER_BOUND('',#1128,.T.);
#699=FACE_OUTER_BOUND('',#1129,.T.);
#700=FACE_OUTER_BOUND('',#1130,.T.);
#701=FACE_OUTER_BOUND('',#1131,.T.);
#702=FACE_OUTER_BOUND('',#1132,.T.);
#703=FACE_OUTER_BOUND('',#1133,.T.);
#704=FACE_OUTER_BOUND('',#1134,.T.);
#705=FACE_OUTER_BOUND('',#1135,.T.);
#706=FACE_OUTER_BOUND('',#1136,.T.);
#707=FACE_OUTER_BOUND('',#1137,.T.);
#708=FACE_OUTER_BOUND('',#1138,.T.);
#709=FACE_OUTER_BOUND('',#1139,.T.);
#710=FACE_OUTER_BOUND('',#1140,.T.);
#711=FACE_OUTER_BOUND('',#1141,.T.);
#712=FACE_OUTER_BOUND('',#1142,.T.);
#713=FACE_OUTER_BOUND('',#1143,.T.);
#714=FACE_OUTER_BOUND('',#1144,.T.);
#715=FACE_OUTER_BOUND('',#1145,.T.);
#716=FACE_OUTER_BOUND('',#1146,.T.);
#717=FACE_OUTER_BOUND('',#1147,.T.);
#718=FACE_OUTER_BOUND('',#1148,.T.);
#719=FACE_OUTER_BOUND('',#1149,.T.);
#720=FACE_OUTER_BOUND('',#1150,.T.);
#721=FACE_OUTER_BOUND('',#1151,.T.);
#722=FACE_OUTER_BOUND('',#1152,.T.);
#723=FACE_OUTER_BOUND('',#1153,.T.);
#724=FACE_OUTER_BOUND('',#1154,.T.);
#725=FACE_OUTER_BOUND('',#1155,.T.);
#726=FACE_OUTER_BOUND('',#1156,.T.);
#727=FACE_OUTER_BOUND('',#1157,.T.);
#728=FACE_OUTER_BOUND('',#1158,.T.);
#729=FACE_OUTER_BOUND('',#1159,.T.);
#730=FACE_OUTER_BOUND('',#1160,.T.);
#731=FACE_OUTER_BOUND('',#1161,.T.);
#732=FACE_OUTER_BOUND('',#1162,.T.);
#733=FACE_OUTER_BOUND('',#1163,.T.);
#734=FACE_OUTER_BOUND('',#1164,.T.);
#735=FACE_OUTER_BOUND('',#1165,.T.);
#736=FACE_OUTER_BOUND('',#1166,.T.);
#737=FACE_OUTER_BOUND('',#1167,.T.);
#738=FACE_OUTER_BOUND('',#1168,.T.);
#739=FACE_OUTER_BOUND('',#1169,.T.);
#740=FACE_OUTER_BOUND('',#1170,.T.);
#741=FACE_OUTER_BOUND('',#1171,.T.);
#742=FACE_OUTER_BOUND('',#1172,.T.);
#743=FACE_OUTER_BOUND('',#1173,.T.);
#744=FACE_OUTER_BOUND('',#1174,.T.);
#745=FACE_OUTER_BOUND('',#1175,.T.);
#746=FACE_OUTER_BOUND('',#1176,.T.);
#747=FACE_OUTER_BOUND('',#1177,.T.);
#748=FACE_OUTER_BOUND('',#1178,.T.);
#749=FACE_OUTER_BOUND('',#1179,.T.);
#750=FACE_OUTER_BOUND('',#1180,.T.);
#751=FACE_OUTER_BOUND('',#1181,.T.);
#752=FACE_OUTER_BOUND('',#1182,.T.);
#753=FACE_OUTER_BOUND('',#1183,.T.);
#754=FACE_OUTER_BOUND('',#1184,.T.);
#755=FACE_OUTER_BOUND('',#1185,.T.);
#756=FACE_OUTER_BOUND('',#1186,.T.);
#757=FACE_OUTER_BOUND('',#1187,.T.);
#758=FACE_OUTER_BOUND('',#1188,.T.);
#759=FACE_OUTER_BOUND('',#1193,.T.);
#760=FACE_OUTER_BOUND('',#1194,.T.);
#761=FACE_OUTER_BOUND('',#1195,.T.);
#762=FACE_OUTER_BOUND('',#1196,.T.);
#763=FACE_OUTER_BOUND('',#1197,.T.);
#764=FACE_OUTER_BOUND('',#1198,.T.);
#765=FACE_OUTER_BOUND('',#1199,.T.);
#766=FACE_OUTER_BOUND('',#1200,.T.);
#767=FACE_OUTER_BOUND('',#1201,.T.);
#768=FACE_OUTER_BOUND('',#1202,.T.);
#769=FACE_OUTER_BOUND('',#1203,.T.);
#1102=EDGE_LOOP('',(#4756,#4757,#4758,#4759));
#1103=EDGE_LOOP('',(#4760,#4761,#4762,#4763));
#1104=EDGE_LOOP('',(#4764));
#1105=EDGE_LOOP('',(#4765));
#1106=EDGE_LOOP('',(#4766,#4767,#4768,#4769));
#1107=EDGE_LOOP('',(#4770,#4771,#4772,#4773));
#1108=EDGE_LOOP('',(#4774,#4775,#4776,#4777));
#1109=EDGE_LOOP('',(#4778,#4779,#4780,#4781,#4782));
#1110=EDGE_LOOP('',(#4783,#4784,#4785,#4786));
#1111=EDGE_LOOP('',(#4787));
#1112=EDGE_LOOP('',(#4788));
#1113=EDGE_LOOP('',(#4789,#4790,#4791,#4792,#4793));
#1114=EDGE_LOOP('',(#4794,#4795,#4796,#4797,#4798));
#1115=EDGE_LOOP('',(#4799,#4800,#4801,#4802,#4803));
#1116=EDGE_LOOP('',(#4804,#4805,#4806));
#1117=EDGE_LOOP('',(#4807,#4808,#4809));
#1118=EDGE_LOOP('',(#4810,#4811,#4812));
#1119=EDGE_LOOP('',(#4813,#4814,#4815,#4816));
#1120=EDGE_LOOP('',(#4817,#4818,#4819));
#1121=EDGE_LOOP('',(#4820,#4821,#4822,#4823));
#1122=EDGE_LOOP('',(#4824,#4825,#4826));
#1123=EDGE_LOOP('',(#4827,#4828,#4829,#4830));
#1124=EDGE_LOOP('',(#4831,#4832,#4833,#4834));
#1125=EDGE_LOOP('',(#4835,#4836,#4837));
#1126=EDGE_LOOP('',(#4838,#4839,#4840,#4841));
#1127=EDGE_LOOP('',(#4842,#4843,#4844));
#1128=EDGE_LOOP('',(#4845,#4846,#4847,#4848));
#1129=EDGE_LOOP('',(#4849,#4850,#4851));
#1130=EDGE_LOOP('',(#4852,#4853,#4854,#4855));
#1131=EDGE_LOOP('',(#4856,#4857,#4858,#4859));
#1132=EDGE_LOOP('',(#4860,#4861,#4862,#4863));
#1133=EDGE_LOOP('',(#4864,#4865,#4866));
#1134=EDGE_LOOP('',(#4867,#4868,#4869,#4870));
#1135=EDGE_LOOP('',(#4871,#4872,#4873,#4874));
#1136=EDGE_LOOP('',(#4875,#4876,#4877));
#1137=EDGE_LOOP('',(#4878,#4879,#4880,#4881));
#1138=EDGE_LOOP('',(#4882,#4883,#4884));
#1139=EDGE_LOOP('',(#4885,#4886,#4887,#4888));
#1140=EDGE_LOOP('',(#4889,#4890,#4891));
#1141=EDGE_LOOP('',(#4892,#4893,#4894,#4895));
#1142=EDGE_LOOP('',(#4896,#4897,#4898));
#1143=EDGE_LOOP('',(#4899,#4900,#4901,#4902));
#1144=EDGE_LOOP('',(#4903,#4904,#4905,#4906));
#1145=EDGE_LOOP('',(#4907,#4908,#4909));
#1146=EDGE_LOOP('',(#4910,#4911,#4912));
#1147=EDGE_LOOP('',(#4913,#4914,#4915,#4916));
#1148=EDGE_LOOP('',(#4917,#4918,#4919));
#1149=EDGE_LOOP('',(#4920,#4921,#4922,#4923));
#1150=EDGE_LOOP('',(#4924,#4925,#4926,#4927));
#1151=EDGE_LOOP('',(#4928,#4929,#4930,#4931));
#1152=EDGE_LOOP('',(#4932,#4933,#4934,#4935));
#1153=EDGE_LOOP('',(#4936,#4937,#4938,#4939));
#1154=EDGE_LOOP('',(#4940,#4941,#4942));
#1155=EDGE_LOOP('',(#4943,#4944,#4945));
#1156=EDGE_LOOP('',(#4946,#4947,#4948));
#1157=EDGE_LOOP('',(#4949,#4950,#4951,#4952));
#1158=EDGE_LOOP('',(#4953,#4954,#4955));
#1159=EDGE_LOOP('',(#4956,#4957,#4958,#4959));
#1160=EDGE_LOOP('',(#4960,#4961,#4962,#4963));
#1161=EDGE_LOOP('',(#4964,#4965,#4966,#4967));
#1162=EDGE_LOOP('',(#4968,#4969,#4970,#4971));
#1163=EDGE_LOOP('',(#4972,#4973,#4974,#4975));
#1164=EDGE_LOOP('',(#4976,#4977,#4978,#4979));
#1165=EDGE_LOOP('',(#4980,#4981,#4982,#4983));
#1166=EDGE_LOOP('',(#4984,#4985,#4986,#4987));
#1167=EDGE_LOOP('',(#4988,#4989,#4990,#4991));
#1168=EDGE_LOOP('',(#4992,#4993,#4994,#4995));
#1169=EDGE_LOOP('',(#4996,#4997,#4998,#4999));
#1170=EDGE_LOOP('',(#5000,#5001,#5002,#5003));
#1171=EDGE_LOOP('',(#5004,#5005,#5006,#5007));
#1172=EDGE_LOOP('',(#5008,#5009,#5010,#5011));
#1173=EDGE_LOOP('',(#5012,#5013,#5014,#5015));
#1174=EDGE_LOOP('',(#5016,#5017,#5018,#5019));
#1175=EDGE_LOOP('',(#5020,#5021,#5022,#5023));
#1176=EDGE_LOOP('',(#5024,#5025,#5026,#5027));
#1177=EDGE_LOOP('',(#5028,#5029,#5030,#5031));
#1178=EDGE_LOOP('',(#5032,#5033,#5034,#5035));
#1179=EDGE_LOOP('',(#5036,#5037,#5038,#5039));
#1180=EDGE_LOOP('',(#5040,#5041,#5042,#5043));
#1181=EDGE_LOOP('',(#5044,#5045,#5046,#5047));
#1182=EDGE_LOOP('',(#5048,#5049,#5050,#5051));
#1183=EDGE_LOOP('',(#5052,#5053,#5054,#5055));
#1184=EDGE_LOOP('',(#5056,#5057,#5058,#5059));
#1185=EDGE_LOOP('',(#5060,#5061,#5062,#5063));
#1186=EDGE_LOOP('',(#5064,#5065,#5066,#5067));
#1187=EDGE_LOOP('',(#5068,#5069,#5070,#5071));
#1188=EDGE_LOOP('',(#5072,#5073,#5074,#5075));
#1189=EDGE_LOOP('',(#5076));
#1190=EDGE_LOOP('',(#5077));
#1191=EDGE_LOOP('',(#5078));
#1192=EDGE_LOOP('',(#5079));
#1193=EDGE_LOOP('',(#5080,#5081,#5082,#5083));
#1194=EDGE_LOOP('',(#5084,#5085,#5086,#5087));
#1195=EDGE_LOOP('',(#5088,#5089,#5090,#5091));
#1196=EDGE_LOOP('',(#5092,#5093,#5094,#5095));
#1197=EDGE_LOOP('',(#5096,#5097,#5098,#5099));
#1198=EDGE_LOOP('',(#5100,#5101,#5102,#5103));
#1199=EDGE_LOOP('',(#5104,#5105,#5106,#5107,#5108,#5109,#5110,#5111,#5112,
#5113,#5114,#5115,#5116,#5117,#5118,#5119,#5120,#5121));
#1200=EDGE_LOOP('',(#5122,#5123,#5124,#5125));
#1201=EDGE_LOOP('',(#5126,#5127,#5128,#5129,#5130,#5131,#5132,#5133,#5134,
#5135,#5136,#5137,#5138,#5139,#5140,#5141,#5142,#5143));
#1202=EDGE_LOOP('',(#5144,#5145,#5146,#5147));
#1203=EDGE_LOOP('',(#5148,#5149,#5150,#5151));
#1446=LINE('',#10113,#1776);
#1447=LINE('',#10115,#1777);
#1448=LINE('',#10117,#1778);
#1449=LINE('',#10118,#1779);
#1450=LINE('',#10123,#1780);
#1451=LINE('',#10131,#1781);
#1452=LINE('',#10144,#1782);
#1453=LINE('',#10146,#1783);
#1454=LINE('',#10148,#1784);
#1455=LINE('',#10149,#1785);
#1456=LINE('',#10154,#1786);
#1457=LINE('',#10164,#1787);
#1458=LINE('',#10188,#1788);
#1459=LINE('',#10189,#1789);
#1460=LINE('',#10197,#1790);
#1461=LINE('',#10198,#1791);
#1462=LINE('',#10207,#1792);
#1463=LINE('',#10208,#1793);
#1464=LINE('',#10210,#1794);
#1465=LINE('',#10211,#1795);
#1466=LINE('',#10219,#1796);
#1467=LINE('',#10220,#1797);
#1468=LINE('',#10242,#1798);
#1469=LINE('',#10267,#1799);
#1470=LINE('',#10268,#1800);
#1471=LINE('',#10285,#1801);
#1472=LINE('',#10286,#1802);
#1473=LINE('',#10295,#1803);
#1474=LINE('',#10296,#1804);
#1475=LINE('',#10305,#1805);
#1476=LINE('',#10306,#1806);
#1477=LINE('',#10315,#1807);
#1478=LINE('',#10316,#1808);
#1479=LINE('',#10318,#1809);
#1480=LINE('',#10319,#1810);
#1481=LINE('',#10336,#1811);
#1482=LINE('',#10338,#1812);
#1483=LINE('',#10361,#1813);
#1484=LINE('',#10362,#1814);
#1485=LINE('',#10364,#1815);
#1486=LINE('',#10365,#1816);
#1487=LINE('',#10368,#1817);
#1488=LINE('',#10370,#1818);
#1489=LINE('',#10387,#1819);
#1490=LINE('',#10389,#1820);
#1491=LINE('',#10406,#1821);
#1492=LINE('',#10408,#1822);
#1493=LINE('',#10445,#1823);
#1494=LINE('',#10446,#1824);
#1495=LINE('',#10456,#1825);
#1496=LINE('',#10458,#1826);
#1497=LINE('',#10474,#1827);
#1498=LINE('',#10475,#1828);
#1499=LINE('',#10477,#1829);
#1500=LINE('',#10478,#1830);
#1501=LINE('',#10481,#1831);
#1502=LINE('',#10483,#1832);
#1503=LINE('',#10499,#1833);
#1504=LINE('',#10500,#1834);
#1505=LINE('',#10503,#1835);
#1506=LINE('',#10505,#1836);
#1507=LINE('',#10525,#1837);
#1508=LINE('',#10527,#1838);
#1509=LINE('',#10552,#1839);
#1510=LINE('',#10553,#1840);
#1511=LINE('',#10555,#1841);
#1512=LINE('',#10556,#1842);
#1513=LINE('',#10558,#1843);
#1514=LINE('',#10559,#1844);
#1515=LINE('',#10561,#1845);
#1516=LINE('',#10562,#1846);
#1517=LINE('',#10564,#1847);
#1518=LINE('',#10566,#1848);
#1519=LINE('',#10568,#1849);
#1520=LINE('',#10570,#1850);
#1521=LINE('',#10572,#1851);
#1522=LINE('',#10574,#1852);
#1523=LINE('',#10575,#1853);
#1524=LINE('',#10577,#1854);
#1525=LINE('',#10579,#1855);
#1526=LINE('',#10580,#1856);
#1527=LINE('',#10582,#1857);
#1528=LINE('',#10584,#1858);
#1529=LINE('',#10585,#1859);
#1530=LINE('',#10587,#1860);
#1531=LINE('',#10589,#1861);
#1532=LINE('',#10591,#1862);
#1533=LINE('',#10592,#1863);
#1776=VECTOR('',#8260,10.);
#1777=VECTOR('',#8261,10.);
#1778=VECTOR('',#8262,10.);
#1779=VECTOR('',#8263,10.);
#1780=VECTOR('',#8268,1.99999999999999);
#1781=VECTOR('',#8279,1.99999999999999);
#1782=VECTOR('',#8294,10.);
#1783=VECTOR('',#8295,10.);
#1784=VECTOR('',#8296,10.);
#1785=VECTOR('',#8297,10.);
#1786=VECTOR('',#8302,1.99999999999999);
#1787=VECTOR('',#8315,1.99999999999999);
#1788=VECTOR('',#8344,10.);
#1789=VECTOR('',#8345,10.);
#1790=VECTOR('',#8356,10.);
#1791=VECTOR('',#8357,10.);
#1792=VECTOR('',#8368,10.);
#1793=VECTOR('',#8369,10.);
#1794=VECTOR('',#8372,10.);
#1795=VECTOR('',#8373,10.);
#1796=VECTOR('',#8384,10.);
#1797=VECTOR('',#8385,10.);
#1798=VECTOR('',#8414,10.);
#1799=VECTOR('',#8445,10.);
#1800=VECTOR('',#8446,10.);
#1801=VECTOR('',#8467,10.);
#1802=VECTOR('',#8468,10.);
#1803=VECTOR('',#8479,10.);
#1804=VECTOR('',#8480,10.);
#1805=VECTOR('',#8491,10.);
#1806=VECTOR('',#8492,10.);
#1807=VECTOR('',#8503,10.);
#1808=VECTOR('',#8504,10.);
#1809=VECTOR('',#8507,10.);
#1810=VECTOR('',#8508,10.);
#1811=VECTOR('',#8527,10.);
#1812=VECTOR('',#8528,10.);
#1813=VECTOR('',#8539,10.);
#1814=VECTOR('',#8540,10.);
#1815=VECTOR('',#8543,10.);
#1816=VECTOR('',#8544,10.);
#1817=VECTOR('',#8547,10.);
#1818=VECTOR('',#8548,10.);
#1819=VECTOR('',#8551,10.);
#1820=VECTOR('',#8552,10.);
#1821=VECTOR('',#8555,10.);
#1822=VECTOR('',#8556,10.);
#1823=VECTOR('',#8583,10.);
#1824=VECTOR('',#8584,10.);
#1825=VECTOR('',#8595,10.);
#1826=VECTOR('',#8596,10.);
#1827=VECTOR('',#8599,10.);
#1828=VECTOR('',#8600,10.);
#1829=VECTOR('',#8603,10.);
#1830=VECTOR('',#8604,10.);
#1831=VECTOR('',#8607,10.);
#1832=VECTOR('',#8608,10.);
#1833=VECTOR('',#8611,10.);
#1834=VECTOR('',#8612,10.);
#1835=VECTOR('',#8615,10.);
#1836=VECTOR('',#8616,10.);
#1837=VECTOR('',#8625,10.);
#1838=VECTOR('',#8626,10.);
#1839=VECTOR('',#8647,10.);
#1840=VECTOR('',#8648,10.);
#1841=VECTOR('',#8651,10.);
#1842=VECTOR('',#8652,10.);
#1843=VECTOR('',#8655,10.);
#1844=VECTOR('',#8656,10.);
#1845=VECTOR('',#8659,10.);
#1846=VECTOR('',#8660,10.);
#1847=VECTOR('',#8663,10.);
#1848=VECTOR('',#8666,10.);
#1849=VECTOR('',#8669,10.);
#1850=VECTOR('',#8672,10.);
#1851=VECTOR('',#8675,10.);
#1852=VECTOR('',#8678,10.);
#1853=VECTOR('',#8679,10.);
#1854=VECTOR('',#8682,10.);
#1855=VECTOR('',#8685,10.);
#1856=VECTOR('',#8686,10.);
#1857=VECTOR('',#8689,10.);
#1858=VECTOR('',#8692,10.);
#1859=VECTOR('',#8693,10.);
#1860=VECTOR('',#8696,10.);
#1861=VECTOR('',#8699,10.);
#1862=VECTOR('',#8702,10.);
#1863=VECTOR('',#8703,10.);
#2200=CIRCLE('',#6491,1.99999999999999);
#2201=CIRCLE('',#6492,0.3);
#2202=CIRCLE('',#6493,2.29999999999999);
#2203=CIRCLE('',#6495,2.29999999999999);
#2204=CIRCLE('',#6497,1.99999999999999);
#2205=CIRCLE('',#6499,1.99999999999999);
#2206=CIRCLE('',#6500,0.3);
#2207=CIRCLE('',#6502,1.99999999999999);
#2208=CIRCLE('',#6504,2.29999999999999);
#2209=CIRCLE('',#6505,0.3);
#2210=CIRCLE('',#6506,1.99999999999999);
#2211=CIRCLE('',#6507,1.99999999999999);
#2212=CIRCLE('',#6509,2.29999999999999);
#2213=CIRCLE('',#6511,1.99999999999999);
#2214=CIRCLE('',#6513,0.3);
#2215=CIRCLE('',#6514,1.99999999999999);
#2216=CIRCLE('',#6515,1.99999999999999);
#2217=CIRCLE('',#6517,1.99999999999999);
#2218=CIRCLE('',#6519,0.299999999999994);
#2219=CIRCLE('',#6520,0.3);
#2220=CIRCLE('',#6521,0.299999999999998);
#2221=CIRCLE('',#6523,0.300000000000002);
#2222=CIRCLE('',#6524,0.299999999999994);
#2223=CIRCLE('',#6525,0.299999999999994);
#2224=CIRCLE('',#6527,0.3);
#2225=CIRCLE('',#6528,0.300000000000011);
#2226=CIRCLE('',#6529,0.299999999999998);
#2227=CIRCLE('',#6532,0.299999999999994);
#2228=CIRCLE('',#6533,0.299999999999998);
#2229=CIRCLE('',#6534,0.299999999999998);
#2230=CIRCLE('',#6537,0.299999999999994);
#2231=CIRCLE('',#6538,0.3);
#2232=CIRCLE('',#6539,0.299999999999998);
#2233=CIRCLE('',#6543,0.299999999999998);
#2234=CIRCLE('',#6544,0.299999999999994);
#2235=CIRCLE('',#6545,0.3);
#2236=CIRCLE('',#6548,0.299999999999994);
#2237=CIRCLE('',#6549,0.3);
#2238=CIRCLE('',#6550,0.299999999999994);
#2239=CIRCLE('',#6552,0.299999999999998);
#2240=CIRCLE('',#6553,0.299999999999994);
#2241=CIRCLE('',#6554,0.599999999999996);
#2242=CIRCLE('',#6555,0.3);
#2243=CIRCLE('',#6557,0.299999999999994);
#2244=CIRCLE('',#6558,0.3);
#2245=CIRCLE('',#6559,0.299999999999994);
#2246=CIRCLE('',#6562,0.600000000000001);
#2247=CIRCLE('',#6563,0.299999999999998);
#2248=CIRCLE('',#6564,0.3);
#2249=CIRCLE('',#6565,0.299999999999994);
#2250=CIRCLE('',#6567,0.600000000000001);
#2251=CIRCLE('',#6568,0.299999999999994);
#2252=CIRCLE('',#6569,0.3);
#2253=CIRCLE('',#6570,0.299999999999976);
#2254=CIRCLE('',#6572,0.300000000000011);
#2255=CIRCLE('',#6573,0.299999999999998);
#2256=CIRCLE('',#6574,0.3);
#2257=CIRCLE('',#6577,0.299999999999994);
#2258=CIRCLE('',#6578,0.299999999999994);
#2259=CIRCLE('',#6579,0.599999999999987);
#2260=CIRCLE('',#6580,0.3);
#2261=CIRCLE('',#6582,0.299999999999998);
#2262=CIRCLE('',#6583,0.299999999999994);
#2263=CIRCLE('',#6584,0.3);
#2264=CIRCLE('',#6587,0.300000000000002);
#2265=CIRCLE('',#6588,0.299999999999994);
#2266=CIRCLE('',#6589,0.3);
#2267=CIRCLE('',#6592,0.299999999999994);
#2268=CIRCLE('',#6593,0.3);
#2269=CIRCLE('',#6594,0.299999999999998);
#2270=CIRCLE('',#6597,0.299999999999994);
#2271=CIRCLE('',#6598,0.299999999999994);
#2272=CIRCLE('',#6599,0.3);
#2273=CIRCLE('',#6603,0.299999999999994);
#2274=CIRCLE('',#6604,0.299999999999998);
#2275=CIRCLE('',#6605,0.300000000000002);
#2276=CIRCLE('',#6607,0.299999999999998);
#2277=CIRCLE('',#6608,0.300000000000002);
#2278=CIRCLE('',#6609,0.300000000000011);
#2279=CIRCLE('',#6612,0.299999999999994);
#2280=CIRCLE('',#6613,0.3);
#2281=CIRCLE('',#6614,0.299999999999998);
#2282=CIRCLE('',#6621,0.299999999999998);
#2283=CIRCLE('',#6622,0.3);
#2284=CIRCLE('',#6623,0.300000000000011);
#2285=CIRCLE('',#6625,0.299999999999994);
#2286=CIRCLE('',#6626,0.3);
#2287=CIRCLE('',#6627,0.299999999999998);
#2288=CIRCLE('',#6629,0.299999999999994);
#2289=CIRCLE('',#6630,0.3);
#2290=CIRCLE('',#6631,0.299999999999998);
#2291=CIRCLE('',#6634,0.299999999999994);
#2292=CIRCLE('',#6635,0.299999999999994);
#2293=CIRCLE('',#6636,0.3);
#2294=CIRCLE('',#6644,4.);
#2295=CIRCLE('',#6645,4.3);
#2296=CIRCLE('',#6648,4.3);
#2297=CIRCLE('',#6649,4.);
#2298=CIRCLE('',#6651,4.3);
#2299=CIRCLE('',#6652,4.);
#2300=CIRCLE('',#6654,4.);
#2301=CIRCLE('',#6655,4.3);
#2646=VERTEX_POINT('',#10105);
#2647=VERTEX_POINT('',#10107);
#2648=VERTEX_POINT('',#10111);
#2649=VERTEX_POINT('',#10112);
#2650=VERTEX_POINT('',#10114);
#2651=VERTEX_POINT('',#10116);
#2652=VERTEX_POINT('',#10119);
#2653=VERTEX_POINT('',#10122);
#2654=VERTEX_POINT('',#10126);
#2655=VERTEX_POINT('',#10130);
#2656=VERTEX_POINT('',#10134);
#2657=VERTEX_POINT('',#10136);
#2658=VERTEX_POINT('',#10138);
#2659=VERTEX_POINT('',#10142);
#2660=VERTEX_POINT('',#10143);
#2661=VERTEX_POINT('',#10145);
#2662=VERTEX_POINT('',#10147);
#2663=VERTEX_POINT('',#10150);
#2664=VERTEX_POINT('',#10153);
#2665=VERTEX_POINT('',#10157);
#2666=VERTEX_POINT('',#10159);
#2667=VERTEX_POINT('',#10163);
#2668=VERTEX_POINT('',#10167);
#2669=VERTEX_POINT('',#10168);
#2670=VERTEX_POINT('',#10170);
#2671=VERTEX_POINT('',#10174);
#2672=VERTEX_POINT('',#10175);
#2673=VERTEX_POINT('',#10177);
#2674=VERTEX_POINT('',#10181);
#2675=VERTEX_POINT('',#10182);
#2676=VERTEX_POINT('',#10184);
#2677=VERTEX_POINT('',#10191);
#2678=VERTEX_POINT('',#10193);
#2679=VERTEX_POINT('',#10200);
#2680=VERTEX_POINT('',#10201);
#2681=VERTEX_POINT('',#10203);
#2682=VERTEX_POINT('',#10213);
#2683=VERTEX_POINT('',#10215);
#2684=VERTEX_POINT('',#10222);
#2685=VERTEX_POINT('',#10223);
#2686=VERTEX_POINT('',#10228);
#2687=VERTEX_POINT('',#10230);
#2688=VERTEX_POINT('',#10232);
#2689=VERTEX_POINT('',#10236);
#2690=VERTEX_POINT('',#10237);
#2691=VERTEX_POINT('',#10244);
#2692=VERTEX_POINT('',#10245);
#2693=VERTEX_POINT('',#10247);
#2694=VERTEX_POINT('',#10252);
#2695=VERTEX_POINT('',#10253);
#2696=VERTEX_POINT('',#10255);
#2697=VERTEX_POINT('',#10260);
#2698=VERTEX_POINT('',#10261);
#2699=VERTEX_POINT('',#10263);
#2700=VERTEX_POINT('',#10270);
#2701=VERTEX_POINT('',#10272);
#2702=VERTEX_POINT('',#10274);
#2703=VERTEX_POINT('',#10278);
#2704=VERTEX_POINT('',#10279);
#2705=VERTEX_POINT('',#10281);
#2706=VERTEX_POINT('',#10288);
#2707=VERTEX_POINT('',#10289);
#2708=VERTEX_POINT('',#10291);
#2709=VERTEX_POINT('',#10298);
#2710=VERTEX_POINT('',#10299);
#2711=VERTEX_POINT('',#10301);
#2712=VERTEX_POINT('',#10308);
#2713=VERTEX_POINT('',#10309);
#2714=VERTEX_POINT('',#10311);
#2715=VERTEX_POINT('',#10321);
#2716=VERTEX_POINT('',#10322);
#2717=VERTEX_POINT('',#10324);
#2718=VERTEX_POINT('',#10328);
#2719=VERTEX_POINT('',#10329);
#2720=VERTEX_POINT('',#10331);
#2721=VERTEX_POINT('',#10335);
#2722=VERTEX_POINT('',#10337);
#2723=VERTEX_POINT('',#10354);
#2724=VERTEX_POINT('',#10355);
#2725=VERTEX_POINT('',#10357);
#2726=VERTEX_POINT('',#10367);
#2727=VERTEX_POINT('',#10369);
#2728=VERTEX_POINT('',#10386);
#2729=VERTEX_POINT('',#10388);
#2730=VERTEX_POINT('',#10405);
#2731=VERTEX_POINT('',#10407);
#2732=VERTEX_POINT('',#10424);
#2733=VERTEX_POINT('',#10425);
#2734=VERTEX_POINT('',#10427);
#2735=VERTEX_POINT('',#10431);
#2736=VERTEX_POINT('',#10432);
#2737=VERTEX_POINT('',#10434);
#2738=VERTEX_POINT('',#10438);
#2739=VERTEX_POINT('',#10439);
#2740=VERTEX_POINT('',#10441);
#2741=VERTEX_POINT('',#10448);
#2742=VERTEX_POINT('',#10449);
#2743=VERTEX_POINT('',#10451);
#2744=VERTEX_POINT('',#10455);
#2745=VERTEX_POINT('',#10457);
#2746=VERTEX_POINT('',#10480);
#2747=VERTEX_POINT('',#10482);
#2748=VERTEX_POINT('',#10502);
#2749=VERTEX_POINT('',#10504);
#2750=VERTEX_POINT('',#10524);
#2751=VERTEX_POINT('',#10526);
#3354=EDGE_CURVE('',#2646,#2646,#2200,.T.);
#3355=EDGE_CURVE('',#2646,#2647,#2201,.T.);
#3356=EDGE_CURVE('',#2647,#2647,#2202,.T.);
#3357=EDGE_CURVE('',#2648,#2649,#1446,.T.);
#3358=EDGE_CURVE('',#2650,#2648,#1447,.T.);
#3359=EDGE_CURVE('',#2651,#2650,#1448,.T.);
#3360=EDGE_CURVE('',#2649,#2651,#1449,.T.);
#3361=EDGE_CURVE('',#2652,#2652,#2203,.T.);
#3362=EDGE_CURVE('',#2646,#2653,#1450,.T.);
#3363=EDGE_CURVE('',#2653,#2653,#2204,.T.);
#3364=EDGE_CURVE('',#2654,#2654,#2205,.T.);
#3365=EDGE_CURVE('',#2654,#2652,#2206,.T.);
#3366=EDGE_CURVE('',#2654,#2655,#1451,.T.);
#3367=EDGE_CURVE('',#2655,#2655,#2207,.T.);
#3368=EDGE_CURVE('',#2656,#2656,#2208,.T.);
#3369=EDGE_CURVE('',#2656,#2657,#2209,.T.);
#3370=EDGE_CURVE('',#2657,#2658,#2210,.T.);
#3371=EDGE_CURVE('',#2658,#2657,#2211,.T.);
#3372=EDGE_CURVE('',#2659,#2660,#1452,.T.);
#3373=EDGE_CURVE('',#2661,#2659,#1453,.T.);
#3374=EDGE_CURVE('',#2662,#2661,#1454,.T.);
#3375=EDGE_CURVE('',#2660,#2662,#1455,.T.);
#3376=EDGE_CURVE('',#2663,#2663,#2212,.T.);
#3377=EDGE_CURVE('',#2658,#2664,#1456,.T.);
#3378=EDGE_CURVE('',#2664,#2664,#2213,.T.);
#3379=EDGE_CURVE('',#2663,#2665,#2214,.T.);
#3380=EDGE_CURVE('',#2665,#2666,#2215,.T.);
#3381=EDGE_CURVE('',#2666,#2665,#2216,.T.);
#3382=EDGE_CURVE('',#2666,#2667,#1457,.T.);
#3383=EDGE_CURVE('',#2667,#2667,#2217,.T.);
#3384=EDGE_CURVE('',#2668,#2669,#2218,.F.);
#3385=EDGE_CURVE('',#2670,#2668,#2219,.F.);
#3386=EDGE_CURVE('',#2669,#2670,#2220,.F.);
#3387=EDGE_CURVE('',#2671,#2672,#2221,.F.);
#3388=EDGE_CURVE('',#2673,#2671,#2222,.F.);
#3389=EDGE_CURVE('',#2672,#2673,#2223,.F.);
#3390=EDGE_CURVE('',#2674,#2675,#2224,.F.);
#3391=EDGE_CURVE('',#2676,#2674,#2225,.F.);
#3392=EDGE_CURVE('',#2675,#2676,#2226,.F.);
#3393=EDGE_CURVE('',#2674,#2670,#1458,.T.);
#3394=EDGE_CURVE('',#2668,#2676,#1459,.T.);
#3395=EDGE_CURVE('',#2677,#2661,#2227,.F.);
#3396=EDGE_CURVE('',#2678,#2677,#2228,.F.);
#3397=EDGE_CURVE('',#2661,#2678,#2229,.F.);
#3398=EDGE_CURVE('',#2677,#2668,#1460,.T.);
#3399=EDGE_CURVE('',#2669,#2678,#1461,.T.);
#3400=EDGE_CURVE('',#2679,#2680,#2230,.F.);
#3401=EDGE_CURVE('',#2681,#2679,#2231,.F.);
#3402=EDGE_CURVE('',#2680,#2681,#2232,.F.);
#3403=EDGE_CURVE('',#2679,#2673,#1462,.T.);
#3404=EDGE_CURVE('',#2671,#2681,#1463,.T.);
#3405=EDGE_CURVE('',#2675,#2680,#1464,.T.);
#3406=EDGE_CURVE('',#2681,#2674,#1465,.T.);
#3407=EDGE_CURVE('',#2682,#2662,#2233,.F.);
#3408=EDGE_CURVE('',#2683,#2682,#2234,.F.);
#3409=EDGE_CURVE('',#2662,#2683,#2235,.F.);
#3410=EDGE_CURVE('',#2682,#2672,#1466,.T.);
#3411=EDGE_CURVE('',#2673,#2683,#1467,.T.);
#3412=EDGE_CURVE('',#2684,#2685,#2236,.F.);
#3413=EDGE_CURVE('',#2648,#2684,#2237,.F.);
#3414=EDGE_CURVE('',#2685,#2648,#2238,.F.);
#3415=EDGE_CURVE('',#2686,#2659,#2239,.F.);
#3416=EDGE_CURVE('',#2687,#2686,#2240,.T.);
#3417=EDGE_CURVE('',#2687,#2688,#2241,.T.);
#3418=EDGE_CURVE('',#2659,#2688,#2242,.T.);
#3419=EDGE_CURVE('',#2689,#2690,#2243,.F.);
#3420=EDGE_CURVE('',#2649,#2689,#2244,.F.);
#3421=EDGE_CURVE('',#2690,#2649,#2245,.F.);
#3422=EDGE_CURVE('',#2689,#2685,#1468,.T.);
#3423=EDGE_CURVE('',#2691,#2692,#2246,.T.);
#3424=EDGE_CURVE('',#2693,#2692,#2247,.T.);
#3425=EDGE_CURVE('',#2660,#2693,#2248,.F.);
#3426=EDGE_CURVE('',#2691,#2660,#2249,.T.);
#3427=EDGE_CURVE('',#2694,#2695,#2250,.T.);
#3428=EDGE_CURVE('',#2696,#2695,#2251,.T.);
#3429=EDGE_CURVE('',#2650,#2696,#2252,.F.);
#3430=EDGE_CURVE('',#2694,#2650,#2253,.T.);
#3431=EDGE_CURVE('',#2697,#2698,#2254,.F.);
#3432=EDGE_CURVE('',#2699,#2697,#2255,.F.);
#3433=EDGE_CURVE('',#2698,#2699,#2256,.F.);
#3434=EDGE_CURVE('',#2686,#2699,#1469,.T.);
#3435=EDGE_CURVE('',#2697,#2687,#1470,.T.);
#3436=EDGE_CURVE('',#2700,#2651,#2257,.F.);
#3437=EDGE_CURVE('',#2701,#2700,#2258,.T.);
#3438=EDGE_CURVE('',#2701,#2702,#2259,.T.);
#3439=EDGE_CURVE('',#2651,#2702,#2260,.T.);
#3440=EDGE_CURVE('',#2703,#2704,#2261,.F.);
#3441=EDGE_CURVE('',#2705,#2703,#2262,.F.);
#3442=EDGE_CURVE('',#2704,#2705,#2263,.F.);
#3443=EDGE_CURVE('',#2703,#2693,#1471,.T.);
#3444=EDGE_CURVE('',#2692,#2705,#1472,.T.);
#3445=EDGE_CURVE('',#2706,#2707,#2264,.F.);
#3446=EDGE_CURVE('',#2708,#2706,#2265,.F.);
#3447=EDGE_CURVE('',#2707,#2708,#2266,.F.);
#3448=EDGE_CURVE('',#2706,#2696,#1473,.T.);
#3449=EDGE_CURVE('',#2695,#2708,#1474,.T.);
#3450=EDGE_CURVE('',#2709,#2710,#2267,.F.);
#3451=EDGE_CURVE('',#2711,#2709,#2268,.F.);
#3452=EDGE_CURVE('',#2710,#2711,#2269,.F.);
#3453=EDGE_CURVE('',#2698,#2711,#1475,.T.);
#3454=EDGE_CURVE('',#2709,#2697,#1476,.T.);
#3455=EDGE_CURVE('',#2712,#2713,#2270,.F.);
#3456=EDGE_CURVE('',#2714,#2712,#2271,.F.);
#3457=EDGE_CURVE('',#2713,#2714,#2272,.F.);
#3458=EDGE_CURVE('',#2712,#2701,#1477,.T.);
#3459=EDGE_CURVE('',#2700,#2714,#1478,.T.);
#3460=EDGE_CURVE('',#2707,#2713,#1479,.T.);
#3461=EDGE_CURVE('',#2714,#2706,#1480,.T.);
#3462=EDGE_CURVE('',#2715,#2716,#2273,.F.);
#3463=EDGE_CURVE('',#2717,#2715,#2274,.F.);
#3464=EDGE_CURVE('',#2716,#2717,#2275,.F.);
#3465=EDGE_CURVE('',#2718,#2719,#2276,.F.);
#3466=EDGE_CURVE('',#2720,#2718,#2277,.F.);
#3467=EDGE_CURVE('',#2719,#2720,#2278,.F.);
#3468=EDGE_CURVE('',#2721,#2709,#1481,.T.);
#3469=EDGE_CURVE('',#2710,#2722,#1482,.T.);
#3470=EDGE_CURVE('',#2722,#2721,#59,.T.);
#3471=EDGE_CURVE('',#2723,#2724,#2279,.F.);
#3472=EDGE_CURVE('',#2725,#2723,#2280,.F.);
#3473=EDGE_CURVE('',#2724,#2725,#2281,.F.);
#3474=EDGE_CURVE('',#2713,#2725,#1483,.T.);
#3475=EDGE_CURVE('',#2723,#2712,#1484,.T.);
#3476=EDGE_CURVE('',#2725,#2720,#1485,.T.);
#3477=EDGE_CURVE('',#2718,#2724,#1486,.T.);
#3478=EDGE_CURVE('',#2726,#2717,#1487,.T.);
#3479=EDGE_CURVE('',#2715,#2727,#1488,.T.);
#3480=EDGE_CURVE('',#2727,#2726,#60,.T.);
#3481=EDGE_CURVE('',#2728,#2718,#1489,.T.);
#3482=EDGE_CURVE('',#2719,#2729,#1490,.T.);
#3483=EDGE_CURVE('',#2729,#2728,#61,.T.);
#3484=EDGE_CURVE('',#2730,#2723,#1491,.T.);
#3485=EDGE_CURVE('',#2724,#2731,#1492,.T.);
#3486=EDGE_CURVE('',#2731,#2730,#62,.T.);
#3487=EDGE_CURVE('',#2732,#2733,#2282,.F.);
#3488=EDGE_CURVE('',#2734,#2732,#2283,.F.);
#3489=EDGE_CURVE('',#2733,#2734,#2284,.F.);
#3490=EDGE_CURVE('',#2735,#2736,#2285,.F.);
#3491=EDGE_CURVE('',#2737,#2735,#2286,.F.);
#3492=EDGE_CURVE('',#2736,#2737,#2287,.F.);
#3493=EDGE_CURVE('',#2738,#2739,#2288,.F.);
#3494=EDGE_CURVE('',#2740,#2738,#2289,.F.);
#3495=EDGE_CURVE('',#2739,#2740,#2290,.F.);
#3496=EDGE_CURVE('',#2734,#2740,#1493,.T.);
#3497=EDGE_CURVE('',#2738,#2733,#1494,.T.);
#3498=EDGE_CURVE('',#2741,#2742,#2291,.F.);
#3499=EDGE_CURVE('',#2743,#2741,#2292,.F.);
#3500=EDGE_CURVE('',#2742,#2743,#2293,.F.);
#3501=EDGE_CURVE('',#2744,#2743,#1495,.T.);
#3502=EDGE_CURVE('',#2741,#2745,#1496,.T.);
#3503=EDGE_CURVE('',#2745,#2744,#63,.T.);
#3504=EDGE_CURVE('',#2740,#2742,#1497,.T.);
#3505=EDGE_CURVE('',#2743,#2739,#1498,.T.);
#3506=EDGE_CURVE('',#2742,#2737,#1499,.T.);
#3507=EDGE_CURVE('',#2735,#2741,#1500,.T.);
#3508=EDGE_CURVE('',#2746,#2738,#1501,.T.);
#3509=EDGE_CURVE('',#2739,#2747,#1502,.T.);
#3510=EDGE_CURVE('',#2747,#2746,#64,.T.);
#3511=EDGE_CURVE('',#2737,#2734,#1503,.T.);
#3512=EDGE_CURVE('',#2732,#2736,#1504,.T.);
#3513=EDGE_CURVE('',#2748,#2735,#1505,.T.);
#3514=EDGE_CURVE('',#2736,#2749,#1506,.T.);
#3515=EDGE_CURVE('',#2749,#2748,#65,.T.);
#3516=EDGE_CURVE('',#2731,#2744,#2294,.T.);
#3517=EDGE_CURVE('',#2745,#2730,#2295,.T.);
#3518=EDGE_CURVE('',#2750,#2732,#1507,.T.);
#3519=EDGE_CURVE('',#2733,#2751,#1508,.T.);
#3520=EDGE_CURVE('',#2751,#2750,#66,.T.);
#3521=EDGE_CURVE('',#2729,#2746,#2296,.T.);
#3522=EDGE_CURVE('',#2747,#2728,#2297,.T.);
#3523=EDGE_CURVE('',#2727,#2748,#2298,.T.);
#3524=EDGE_CURVE('',#2749,#2726,#2299,.T.);
#3525=EDGE_CURVE('',#2722,#2750,#2300,.T.);
#3526=EDGE_CURVE('',#2751,#2721,#2301,.T.);
#3527=EDGE_CURVE('',#2720,#2707,#1509,.T.);
#3528=EDGE_CURVE('',#2708,#2719,#1510,.T.);
#3529=EDGE_CURVE('',#2711,#2716,#1511,.T.);
#3530=EDGE_CURVE('',#2717,#2710,#1512,.T.);
#3531=EDGE_CURVE('',#2716,#2704,#1513,.T.);
#3532=EDGE_CURVE('',#2705,#2715,#1514,.T.);
#3533=EDGE_CURVE('',#2704,#2698,#1515,.T.);
#3534=EDGE_CURVE('',#2699,#2703,#1516,.T.);
#3535=EDGE_CURVE('',#2702,#2690,#1517,.T.);
#3536=EDGE_CURVE('',#2696,#2700,#1518,.T.);
#3537=EDGE_CURVE('',#2684,#2694,#1519,.T.);
#3538=EDGE_CURVE('',#2693,#2686,#1520,.T.);
#3539=EDGE_CURVE('',#2683,#2691,#1521,.T.);
#3540=EDGE_CURVE('',#2690,#2679,#1522,.T.);
#3541=EDGE_CURVE('',#2680,#2689,#1523,.T.);
#3542=EDGE_CURVE('',#2688,#2677,#1524,.T.);
#3543=EDGE_CURVE('',#2685,#2675,#1525,.T.);
#3544=EDGE_CURVE('',#2676,#2684,#1526,.T.);
#3545=EDGE_CURVE('',#2678,#2682,#1527,.T.);
#3546=EDGE_CURVE('',#2670,#2671,#1528,.T.);
#3547=EDGE_CURVE('',#2672,#2669,#1529,.T.);
#3548=EDGE_CURVE('',#2747,#2744,#1530,.T.);
#3549=EDGE_CURVE('',#2728,#2731,#1531,.T.);
#3550=EDGE_CURVE('',#2750,#2749,#1532,.T.);
#3551=EDGE_CURVE('',#2722,#2726,#1533,.T.);
#4756=ORIENTED_EDGE('',*,*,#3354,.T.);
#4757=ORIENTED_EDGE('',*,*,#3355,.T.);
#4758=ORIENTED_EDGE('',*,*,#3356,.T.);
#4759=ORIENTED_EDGE('',*,*,#3355,.F.);
#4760=ORIENTED_EDGE('',*,*,#3357,.F.);
#4761=ORIENTED_EDGE('',*,*,#3358,.F.);
#4762=ORIENTED_EDGE('',*,*,#3359,.F.);
#4763=ORIENTED_EDGE('',*,*,#3360,.F.);
#4764=ORIENTED_EDGE('',*,*,#3361,.F.);
#4765=ORIENTED_EDGE('',*,*,#3356,.F.);
#4766=ORIENTED_EDGE('',*,*,#3354,.F.);
#4767=ORIENTED_EDGE('',*,*,#3362,.T.);
#4768=ORIENTED_EDGE('',*,*,#3363,.T.);
#4769=ORIENTED_EDGE('',*,*,#3362,.F.);
#4770=ORIENTED_EDGE('',*,*,#3364,.T.);
#4771=ORIENTED_EDGE('',*,*,#3365,.T.);
#4772=ORIENTED_EDGE('',*,*,#3361,.T.);
#4773=ORIENTED_EDGE('',*,*,#3365,.F.);
#4774=ORIENTED_EDGE('',*,*,#3364,.F.);
#4775=ORIENTED_EDGE('',*,*,#3366,.T.);
#4776=ORIENTED_EDGE('',*,*,#3367,.T.);
#4777=ORIENTED_EDGE('',*,*,#3366,.F.);
#4778=ORIENTED_EDGE('',*,*,#3368,.T.);
#4779=ORIENTED_EDGE('',*,*,#3369,.T.);
#4780=ORIENTED_EDGE('',*,*,#3370,.T.);
#4781=ORIENTED_EDGE('',*,*,#3371,.T.);
#4782=ORIENTED_EDGE('',*,*,#3369,.F.);
#4783=ORIENTED_EDGE('',*,*,#3372,.F.);
#4784=ORIENTED_EDGE('',*,*,#3373,.F.);
#4785=ORIENTED_EDGE('',*,*,#3374,.F.);
#4786=ORIENTED_EDGE('',*,*,#3375,.F.);
#4787=ORIENTED_EDGE('',*,*,#3376,.F.);
#4788=ORIENTED_EDGE('',*,*,#3368,.F.);
#4789=ORIENTED_EDGE('',*,*,#3371,.F.);
#4790=ORIENTED_EDGE('',*,*,#3377,.T.);
#4791=ORIENTED_EDGE('',*,*,#3378,.F.);
#4792=ORIENTED_EDGE('',*,*,#3377,.F.);
#4793=ORIENTED_EDGE('',*,*,#3370,.F.);
#4794=ORIENTED_EDGE('',*,*,#3376,.T.);
#4795=ORIENTED_EDGE('',*,*,#3379,.T.);
#4796=ORIENTED_EDGE('',*,*,#3380,.T.);
#4797=ORIENTED_EDGE('',*,*,#3381,.T.);
#4798=ORIENTED_EDGE('',*,*,#3379,.F.);
#4799=ORIENTED_EDGE('',*,*,#3381,.F.);
#4800=ORIENTED_EDGE('',*,*,#3382,.T.);
#4801=ORIENTED_EDGE('',*,*,#3383,.F.);
#4802=ORIENTED_EDGE('',*,*,#3382,.F.);
#4803=ORIENTED_EDGE('',*,*,#3380,.F.);
#4804=ORIENTED_EDGE('',*,*,#3384,.F.);
#4805=ORIENTED_EDGE('',*,*,#3385,.F.);
#4806=ORIENTED_EDGE('',*,*,#3386,.F.);
#4807=ORIENTED_EDGE('',*,*,#3387,.F.);
#4808=ORIENTED_EDGE('',*,*,#3388,.F.);
#4809=ORIENTED_EDGE('',*,*,#3389,.F.);
#4810=ORIENTED_EDGE('',*,*,#3390,.F.);
#4811=ORIENTED_EDGE('',*,*,#3391,.F.);
#4812=ORIENTED_EDGE('',*,*,#3392,.F.);
#4813=ORIENTED_EDGE('',*,*,#3391,.T.);
#4814=ORIENTED_EDGE('',*,*,#3393,.T.);
#4815=ORIENTED_EDGE('',*,*,#3385,.T.);
#4816=ORIENTED_EDGE('',*,*,#3394,.T.);
#4817=ORIENTED_EDGE('',*,*,#3395,.F.);
#4818=ORIENTED_EDGE('',*,*,#3396,.F.);
#4819=ORIENTED_EDGE('',*,*,#3397,.F.);
#4820=ORIENTED_EDGE('',*,*,#3396,.T.);
#4821=ORIENTED_EDGE('',*,*,#3398,.T.);
#4822=ORIENTED_EDGE('',*,*,#3384,.T.);
#4823=ORIENTED_EDGE('',*,*,#3399,.T.);
#4824=ORIENTED_EDGE('',*,*,#3400,.F.);
#4825=ORIENTED_EDGE('',*,*,#3401,.F.);
#4826=ORIENTED_EDGE('',*,*,#3402,.F.);
#4827=ORIENTED_EDGE('',*,*,#3401,.T.);
#4828=ORIENTED_EDGE('',*,*,#3403,.T.);
#4829=ORIENTED_EDGE('',*,*,#3388,.T.);
#4830=ORIENTED_EDGE('',*,*,#3404,.T.);
#4831=ORIENTED_EDGE('',*,*,#3390,.T.);
#4832=ORIENTED_EDGE('',*,*,#3405,.T.);
#4833=ORIENTED_EDGE('',*,*,#3402,.T.);
#4834=ORIENTED_EDGE('',*,*,#3406,.T.);
#4835=ORIENTED_EDGE('',*,*,#3407,.F.);
#4836=ORIENTED_EDGE('',*,*,#3408,.F.);
#4837=ORIENTED_EDGE('',*,*,#3409,.F.);
#4838=ORIENTED_EDGE('',*,*,#3408,.T.);
#4839=ORIENTED_EDGE('',*,*,#3410,.T.);
#4840=ORIENTED_EDGE('',*,*,#3389,.T.);
#4841=ORIENTED_EDGE('',*,*,#3411,.T.);
#4842=ORIENTED_EDGE('',*,*,#3412,.F.);
#4843=ORIENTED_EDGE('',*,*,#3413,.F.);
#4844=ORIENTED_EDGE('',*,*,#3414,.F.);
#4845=ORIENTED_EDGE('',*,*,#3415,.F.);
#4846=ORIENTED_EDGE('',*,*,#3416,.F.);
#4847=ORIENTED_EDGE('',*,*,#3417,.T.);
#4848=ORIENTED_EDGE('',*,*,#3418,.F.);
#4849=ORIENTED_EDGE('',*,*,#3419,.F.);
#4850=ORIENTED_EDGE('',*,*,#3420,.F.);
#4851=ORIENTED_EDGE('',*,*,#3421,.F.);
#4852=ORIENTED_EDGE('',*,*,#3420,.T.);
#4853=ORIENTED_EDGE('',*,*,#3422,.T.);
#4854=ORIENTED_EDGE('',*,*,#3414,.T.);
#4855=ORIENTED_EDGE('',*,*,#3357,.T.);
#4856=ORIENTED_EDGE('',*,*,#3423,.T.);
#4857=ORIENTED_EDGE('',*,*,#3424,.F.);
#4858=ORIENTED_EDGE('',*,*,#3425,.F.);
#4859=ORIENTED_EDGE('',*,*,#3426,.F.);
#4860=ORIENTED_EDGE('',*,*,#3427,.T.);
#4861=ORIENTED_EDGE('',*,*,#3428,.F.);
#4862=ORIENTED_EDGE('',*,*,#3429,.F.);
#4863=ORIENTED_EDGE('',*,*,#3430,.F.);
#4864=ORIENTED_EDGE('',*,*,#3431,.F.);
#4865=ORIENTED_EDGE('',*,*,#3432,.F.);
#4866=ORIENTED_EDGE('',*,*,#3433,.F.);
#4867=ORIENTED_EDGE('',*,*,#3416,.T.);
#4868=ORIENTED_EDGE('',*,*,#3434,.T.);
#4869=ORIENTED_EDGE('',*,*,#3432,.T.);
#4870=ORIENTED_EDGE('',*,*,#3435,.T.);
#4871=ORIENTED_EDGE('',*,*,#3436,.F.);
#4872=ORIENTED_EDGE('',*,*,#3437,.F.);
#4873=ORIENTED_EDGE('',*,*,#3438,.T.);
#4874=ORIENTED_EDGE('',*,*,#3439,.F.);
#4875=ORIENTED_EDGE('',*,*,#3440,.F.);
#4876=ORIENTED_EDGE('',*,*,#3441,.F.);
#4877=ORIENTED_EDGE('',*,*,#3442,.F.);
#4878=ORIENTED_EDGE('',*,*,#3441,.T.);
#4879=ORIENTED_EDGE('',*,*,#3443,.T.);
#4880=ORIENTED_EDGE('',*,*,#3424,.T.);
#4881=ORIENTED_EDGE('',*,*,#3444,.T.);
#4882=ORIENTED_EDGE('',*,*,#3445,.F.);
#4883=ORIENTED_EDGE('',*,*,#3446,.F.);
#4884=ORIENTED_EDGE('',*,*,#3447,.F.);
#4885=ORIENTED_EDGE('',*,*,#3446,.T.);
#4886=ORIENTED_EDGE('',*,*,#3448,.T.);
#4887=ORIENTED_EDGE('',*,*,#3428,.T.);
#4888=ORIENTED_EDGE('',*,*,#3449,.T.);
#4889=ORIENTED_EDGE('',*,*,#3450,.F.);
#4890=ORIENTED_EDGE('',*,*,#3451,.F.);
#4891=ORIENTED_EDGE('',*,*,#3452,.F.);
#4892=ORIENTED_EDGE('',*,*,#3431,.T.);
#4893=ORIENTED_EDGE('',*,*,#3453,.T.);
#4894=ORIENTED_EDGE('',*,*,#3451,.T.);
#4895=ORIENTED_EDGE('',*,*,#3454,.T.);
#4896=ORIENTED_EDGE('',*,*,#3455,.F.);
#4897=ORIENTED_EDGE('',*,*,#3456,.F.);
#4898=ORIENTED_EDGE('',*,*,#3457,.F.);
#4899=ORIENTED_EDGE('',*,*,#3456,.T.);
#4900=ORIENTED_EDGE('',*,*,#3458,.T.);
#4901=ORIENTED_EDGE('',*,*,#3437,.T.);
#4902=ORIENTED_EDGE('',*,*,#3459,.T.);
#4903=ORIENTED_EDGE('',*,*,#3445,.T.);
#4904=ORIENTED_EDGE('',*,*,#3460,.T.);
#4905=ORIENTED_EDGE('',*,*,#3457,.T.);
#4906=ORIENTED_EDGE('',*,*,#3461,.T.);
#4907=ORIENTED_EDGE('',*,*,#3462,.F.);
#4908=ORIENTED_EDGE('',*,*,#3463,.F.);
#4909=ORIENTED_EDGE('',*,*,#3464,.F.);
#4910=ORIENTED_EDGE('',*,*,#3465,.F.);
#4911=ORIENTED_EDGE('',*,*,#3466,.F.);
#4912=ORIENTED_EDGE('',*,*,#3467,.F.);
#4913=ORIENTED_EDGE('',*,*,#3468,.T.);
#4914=ORIENTED_EDGE('',*,*,#3450,.T.);
#4915=ORIENTED_EDGE('',*,*,#3469,.T.);
#4916=ORIENTED_EDGE('',*,*,#3470,.T.);
#4917=ORIENTED_EDGE('',*,*,#3471,.F.);
#4918=ORIENTED_EDGE('',*,*,#3472,.F.);
#4919=ORIENTED_EDGE('',*,*,#3473,.F.);
#4920=ORIENTED_EDGE('',*,*,#3455,.T.);
#4921=ORIENTED_EDGE('',*,*,#3474,.T.);
#4922=ORIENTED_EDGE('',*,*,#3472,.T.);
#4923=ORIENTED_EDGE('',*,*,#3475,.T.);
#4924=ORIENTED_EDGE('',*,*,#3473,.T.);
#4925=ORIENTED_EDGE('',*,*,#3476,.T.);
#4926=ORIENTED_EDGE('',*,*,#3466,.T.);
#4927=ORIENTED_EDGE('',*,*,#3477,.T.);
#4928=ORIENTED_EDGE('',*,*,#3478,.T.);
#4929=ORIENTED_EDGE('',*,*,#3463,.T.);
#4930=ORIENTED_EDGE('',*,*,#3479,.T.);
#4931=ORIENTED_EDGE('',*,*,#3480,.T.);
#4932=ORIENTED_EDGE('',*,*,#3481,.T.);
#4933=ORIENTED_EDGE('',*,*,#3465,.T.);
#4934=ORIENTED_EDGE('',*,*,#3482,.T.);
#4935=ORIENTED_EDGE('',*,*,#3483,.T.);
#4936=ORIENTED_EDGE('',*,*,#3484,.T.);
#4937=ORIENTED_EDGE('',*,*,#3471,.T.);
#4938=ORIENTED_EDGE('',*,*,#3485,.T.);
#4939=ORIENTED_EDGE('',*,*,#3486,.T.);
#4940=ORIENTED_EDGE('',*,*,#3487,.F.);
#4941=ORIENTED_EDGE('',*,*,#3488,.F.);
#4942=ORIENTED_EDGE('',*,*,#3489,.F.);
#4943=ORIENTED_EDGE('',*,*,#3490,.F.);
#4944=ORIENTED_EDGE('',*,*,#3491,.F.);
#4945=ORIENTED_EDGE('',*,*,#3492,.F.);
#4946=ORIENTED_EDGE('',*,*,#3493,.F.);
#4947=ORIENTED_EDGE('',*,*,#3494,.F.);
#4948=ORIENTED_EDGE('',*,*,#3495,.F.);
#4949=ORIENTED_EDGE('',*,*,#3489,.T.);
#4950=ORIENTED_EDGE('',*,*,#3496,.T.);
#4951=ORIENTED_EDGE('',*,*,#3494,.T.);
#4952=ORIENTED_EDGE('',*,*,#3497,.T.);
#4953=ORIENTED_EDGE('',*,*,#3498,.F.);
#4954=ORIENTED_EDGE('',*,*,#3499,.F.);
#4955=ORIENTED_EDGE('',*,*,#3500,.F.);
#4956=ORIENTED_EDGE('',*,*,#3501,.T.);
#4957=ORIENTED_EDGE('',*,*,#3499,.T.);
#4958=ORIENTED_EDGE('',*,*,#3502,.T.);
#4959=ORIENTED_EDGE('',*,*,#3503,.T.);
#4960=ORIENTED_EDGE('',*,*,#3495,.T.);
#4961=ORIENTED_EDGE('',*,*,#3504,.T.);
#4962=ORIENTED_EDGE('',*,*,#3500,.T.);
#4963=ORIENTED_EDGE('',*,*,#3505,.T.);
#4964=ORIENTED_EDGE('',*,*,#3498,.T.);
#4965=ORIENTED_EDGE('',*,*,#3506,.T.);
#4966=ORIENTED_EDGE('',*,*,#3491,.T.);
#4967=ORIENTED_EDGE('',*,*,#3507,.T.);
#4968=ORIENTED_EDGE('',*,*,#3508,.T.);
#4969=ORIENTED_EDGE('',*,*,#3493,.T.);
#4970=ORIENTED_EDGE('',*,*,#3509,.T.);
#4971=ORIENTED_EDGE('',*,*,#3510,.T.);
#4972=ORIENTED_EDGE('',*,*,#3492,.T.);
#4973=ORIENTED_EDGE('',*,*,#3511,.T.);
#4974=ORIENTED_EDGE('',*,*,#3488,.T.);
#4975=ORIENTED_EDGE('',*,*,#3512,.T.);
#4976=ORIENTED_EDGE('',*,*,#3513,.T.);
#4977=ORIENTED_EDGE('',*,*,#3490,.T.);
#4978=ORIENTED_EDGE('',*,*,#3514,.T.);
#4979=ORIENTED_EDGE('',*,*,#3515,.T.);
#4980=ORIENTED_EDGE('',*,*,#3516,.T.);
#4981=ORIENTED_EDGE('',*,*,#3503,.F.);
#4982=ORIENTED_EDGE('',*,*,#3517,.T.);
#4983=ORIENTED_EDGE('',*,*,#3486,.F.);
#4984=ORIENTED_EDGE('',*,*,#3518,.T.);
#4985=ORIENTED_EDGE('',*,*,#3487,.T.);
#4986=ORIENTED_EDGE('',*,*,#3519,.T.);
#4987=ORIENTED_EDGE('',*,*,#3520,.T.);
#4988=ORIENTED_EDGE('',*,*,#3521,.T.);
#4989=ORIENTED_EDGE('',*,*,#3510,.F.);
#4990=ORIENTED_EDGE('',*,*,#3522,.T.);
#4991=ORIENTED_EDGE('',*,*,#3483,.F.);
#4992=ORIENTED_EDGE('',*,*,#3523,.T.);
#4993=ORIENTED_EDGE('',*,*,#3515,.F.);
#4994=ORIENTED_EDGE('',*,*,#3524,.T.);
#4995=ORIENTED_EDGE('',*,*,#3480,.F.);
#4996=ORIENTED_EDGE('',*,*,#3525,.T.);
#4997=ORIENTED_EDGE('',*,*,#3520,.F.);
#4998=ORIENTED_EDGE('',*,*,#3526,.T.);
#4999=ORIENTED_EDGE('',*,*,#3470,.F.);
#5000=ORIENTED_EDGE('',*,*,#3467,.T.);
#5001=ORIENTED_EDGE('',*,*,#3527,.T.);
#5002=ORIENTED_EDGE('',*,*,#3447,.T.);
#5003=ORIENTED_EDGE('',*,*,#3528,.T.);
#5004=ORIENTED_EDGE('',*,*,#3452,.T.);
#5005=ORIENTED_EDGE('',*,*,#3529,.T.);
#5006=ORIENTED_EDGE('',*,*,#3464,.T.);
#5007=ORIENTED_EDGE('',*,*,#3530,.T.);
#5008=ORIENTED_EDGE('',*,*,#3462,.T.);
#5009=ORIENTED_EDGE('',*,*,#3531,.T.);
#5010=ORIENTED_EDGE('',*,*,#3442,.T.);
#5011=ORIENTED_EDGE('',*,*,#3532,.T.);
#5012=ORIENTED_EDGE('',*,*,#3440,.T.);
#5013=ORIENTED_EDGE('',*,*,#3533,.T.);
#5014=ORIENTED_EDGE('',*,*,#3433,.T.);
#5015=ORIENTED_EDGE('',*,*,#3534,.T.);
#5016=ORIENTED_EDGE('',*,*,#3439,.T.);
#5017=ORIENTED_EDGE('',*,*,#3535,.T.);
#5018=ORIENTED_EDGE('',*,*,#3421,.T.);
#5019=ORIENTED_EDGE('',*,*,#3360,.T.);
#5020=ORIENTED_EDGE('',*,*,#3429,.T.);
#5021=ORIENTED_EDGE('',*,*,#3536,.T.);
#5022=ORIENTED_EDGE('',*,*,#3436,.T.);
#5023=ORIENTED_EDGE('',*,*,#3359,.T.);
#5024=ORIENTED_EDGE('',*,*,#3413,.T.);
#5025=ORIENTED_EDGE('',*,*,#3537,.T.);
#5026=ORIENTED_EDGE('',*,*,#3430,.T.);
#5027=ORIENTED_EDGE('',*,*,#3358,.T.);
#5028=ORIENTED_EDGE('',*,*,#3425,.T.);
#5029=ORIENTED_EDGE('',*,*,#3538,.T.);
#5030=ORIENTED_EDGE('',*,*,#3415,.T.);
#5031=ORIENTED_EDGE('',*,*,#3372,.T.);
#5032=ORIENTED_EDGE('',*,*,#3426,.T.);
#5033=ORIENTED_EDGE('',*,*,#3375,.T.);
#5034=ORIENTED_EDGE('',*,*,#3409,.T.);
#5035=ORIENTED_EDGE('',*,*,#3539,.T.);
#5036=ORIENTED_EDGE('',*,*,#3419,.T.);
#5037=ORIENTED_EDGE('',*,*,#3540,.T.);
#5038=ORIENTED_EDGE('',*,*,#3400,.T.);
#5039=ORIENTED_EDGE('',*,*,#3541,.T.);
#5040=ORIENTED_EDGE('',*,*,#3395,.T.);
#5041=ORIENTED_EDGE('',*,*,#3373,.T.);
#5042=ORIENTED_EDGE('',*,*,#3418,.T.);
#5043=ORIENTED_EDGE('',*,*,#3542,.T.);
#5044=ORIENTED_EDGE('',*,*,#3412,.T.);
#5045=ORIENTED_EDGE('',*,*,#3543,.T.);
#5046=ORIENTED_EDGE('',*,*,#3392,.T.);
#5047=ORIENTED_EDGE('',*,*,#3544,.T.);
#5048=ORIENTED_EDGE('',*,*,#3407,.T.);
#5049=ORIENTED_EDGE('',*,*,#3374,.T.);
#5050=ORIENTED_EDGE('',*,*,#3397,.T.);
#5051=ORIENTED_EDGE('',*,*,#3545,.T.);
#5052=ORIENTED_EDGE('',*,*,#3386,.T.);
#5053=ORIENTED_EDGE('',*,*,#3546,.T.);
#5054=ORIENTED_EDGE('',*,*,#3387,.T.);
#5055=ORIENTED_EDGE('',*,*,#3547,.T.);
#5056=ORIENTED_EDGE('',*,*,#3509,.F.);
#5057=ORIENTED_EDGE('',*,*,#3505,.F.);
#5058=ORIENTED_EDGE('',*,*,#3501,.F.);
#5059=ORIENTED_EDGE('',*,*,#3548,.F.);
#5060=ORIENTED_EDGE('',*,*,#3522,.F.);
#5061=ORIENTED_EDGE('',*,*,#3548,.T.);
#5062=ORIENTED_EDGE('',*,*,#3516,.F.);
#5063=ORIENTED_EDGE('',*,*,#3549,.F.);
#5064=ORIENTED_EDGE('',*,*,#3524,.F.);
#5065=ORIENTED_EDGE('',*,*,#3550,.F.);
#5066=ORIENTED_EDGE('',*,*,#3525,.F.);
#5067=ORIENTED_EDGE('',*,*,#3551,.T.);
#5068=ORIENTED_EDGE('',*,*,#3514,.F.);
#5069=ORIENTED_EDGE('',*,*,#3512,.F.);
#5070=ORIENTED_EDGE('',*,*,#3518,.F.);
#5071=ORIENTED_EDGE('',*,*,#3550,.T.);
#5072=ORIENTED_EDGE('',*,*,#3404,.F.);
#5073=ORIENTED_EDGE('',*,*,#3546,.F.);
#5074=ORIENTED_EDGE('',*,*,#3393,.F.);
#5075=ORIENTED_EDGE('',*,*,#3406,.F.);
#5076=ORIENTED_EDGE('',*,*,#3383,.T.);
#5077=ORIENTED_EDGE('',*,*,#3378,.T.);
#5078=ORIENTED_EDGE('',*,*,#3367,.F.);
#5079=ORIENTED_EDGE('',*,*,#3363,.F.);
#5080=ORIENTED_EDGE('',*,*,#3410,.F.);
#5081=ORIENTED_EDGE('',*,*,#3545,.F.);
#5082=ORIENTED_EDGE('',*,*,#3399,.F.);
#5083=ORIENTED_EDGE('',*,*,#3547,.F.);
#5084=ORIENTED_EDGE('',*,*,#3422,.F.);
#5085=ORIENTED_EDGE('',*,*,#3541,.F.);
#5086=ORIENTED_EDGE('',*,*,#3405,.F.);
#5087=ORIENTED_EDGE('',*,*,#3543,.F.);
#5088=ORIENTED_EDGE('',*,*,#3443,.F.);
#5089=ORIENTED_EDGE('',*,*,#3534,.F.);
#5090=ORIENTED_EDGE('',*,*,#3434,.F.);
#5091=ORIENTED_EDGE('',*,*,#3538,.F.);
#5092=ORIENTED_EDGE('',*,*,#3453,.F.);
#5093=ORIENTED_EDGE('',*,*,#3533,.F.);
#5094=ORIENTED_EDGE('',*,*,#3531,.F.);
#5095=ORIENTED_EDGE('',*,*,#3529,.F.);
#5096=ORIENTED_EDGE('',*,*,#3459,.F.);
#5097=ORIENTED_EDGE('',*,*,#3536,.F.);
#5098=ORIENTED_EDGE('',*,*,#3448,.F.);
#5099=ORIENTED_EDGE('',*,*,#3461,.F.);
#5100=ORIENTED_EDGE('',*,*,#3460,.F.);
#5101=ORIENTED_EDGE('',*,*,#3527,.F.);
#5102=ORIENTED_EDGE('',*,*,#3476,.F.);
#5103=ORIENTED_EDGE('',*,*,#3474,.F.);
#5104=ORIENTED_EDGE('',*,*,#3497,.F.);
#5105=ORIENTED_EDGE('',*,*,#3508,.F.);
#5106=ORIENTED_EDGE('',*,*,#3521,.F.);
#5107=ORIENTED_EDGE('',*,*,#3482,.F.);
#5108=ORIENTED_EDGE('',*,*,#3528,.F.);
#5109=ORIENTED_EDGE('',*,*,#3449,.F.);
#5110=ORIENTED_EDGE('',*,*,#3427,.F.);
#5111=ORIENTED_EDGE('',*,*,#3537,.F.);
#5112=ORIENTED_EDGE('',*,*,#3544,.F.);
#5113=ORIENTED_EDGE('',*,*,#3394,.F.);
#5114=ORIENTED_EDGE('',*,*,#3398,.F.);
#5115=ORIENTED_EDGE('',*,*,#3542,.F.);
#5116=ORIENTED_EDGE('',*,*,#3417,.F.);
#5117=ORIENTED_EDGE('',*,*,#3435,.F.);
#5118=ORIENTED_EDGE('',*,*,#3454,.F.);
#5119=ORIENTED_EDGE('',*,*,#3468,.F.);
#5120=ORIENTED_EDGE('',*,*,#3526,.F.);
#5121=ORIENTED_EDGE('',*,*,#3519,.F.);
#5122=ORIENTED_EDGE('',*,*,#3496,.F.);
#5123=ORIENTED_EDGE('',*,*,#3511,.F.);
#5124=ORIENTED_EDGE('',*,*,#3506,.F.);
#5125=ORIENTED_EDGE('',*,*,#3504,.F.);
#5126=ORIENTED_EDGE('',*,*,#3502,.F.);
#5127=ORIENTED_EDGE('',*,*,#3507,.F.);
#5128=ORIENTED_EDGE('',*,*,#3513,.F.);
#5129=ORIENTED_EDGE('',*,*,#3523,.F.);
#5130=ORIENTED_EDGE('',*,*,#3479,.F.);
#5131=ORIENTED_EDGE('',*,*,#3532,.F.);
#5132=ORIENTED_EDGE('',*,*,#3444,.F.);
#5133=ORIENTED_EDGE('',*,*,#3423,.F.);
#5134=ORIENTED_EDGE('',*,*,#3539,.F.);
#5135=ORIENTED_EDGE('',*,*,#3411,.F.);
#5136=ORIENTED_EDGE('',*,*,#3403,.F.);
#5137=ORIENTED_EDGE('',*,*,#3540,.F.);
#5138=ORIENTED_EDGE('',*,*,#3535,.F.);
#5139=ORIENTED_EDGE('',*,*,#3438,.F.);
#5140=ORIENTED_EDGE('',*,*,#3458,.F.);
#5141=ORIENTED_EDGE('',*,*,#3475,.F.);
#5142=ORIENTED_EDGE('',*,*,#3484,.F.);
#5143=ORIENTED_EDGE('',*,*,#3517,.F.);
#5144=ORIENTED_EDGE('',*,*,#3481,.F.);
#5145=ORIENTED_EDGE('',*,*,#3549,.T.);
#5146=ORIENTED_EDGE('',*,*,#3485,.F.);
#5147=ORIENTED_EDGE('',*,*,#3477,.F.);
#5148=ORIENTED_EDGE('',*,*,#3478,.F.);
#5149=ORIENTED_EDGE('',*,*,#3551,.F.);
#5150=ORIENTED_EDGE('',*,*,#3469,.F.);
#5151=ORIENTED_EDGE('',*,*,#3530,.F.);
#5280=CYLINDRICAL_SURFACE('',#6496,1.99999999999999);
#5281=CYLINDRICAL_SURFACE('',#6501,1.99999999999999);
#5282=CYLINDRICAL_SURFACE('',#6510,1.99999999999999);
#5283=CYLINDRICAL_SURFACE('',#6516,1.99999999999999);
#5284=CYLINDRICAL_SURFACE('',#6530,0.3);
#5285=CYLINDRICAL_SURFACE('',#6535,0.3);
#5286=CYLINDRICAL_SURFACE('',#6540,0.3);
#5287=CYLINDRICAL_SURFACE('',#6541,0.3);
#5288=CYLINDRICAL_SURFACE('',#6546,0.3);
#5289=CYLINDRICAL_SURFACE('',#6560,0.3);
#5290=CYLINDRICAL_SURFACE('',#6575,0.3);
#5291=CYLINDRICAL_SURFACE('',#6585,0.3);
#5292=CYLINDRICAL_SURFACE('',#6590,0.3);
#5293=CYLINDRICAL_SURFACE('',#6595,0.3);
#5294=CYLINDRICAL_SURFACE('',#6600,0.3);
#5295=CYLINDRICAL_SURFACE('',#6601,0.3);
#5296=CYLINDRICAL_SURFACE('',#6610,0.3);
#5297=CYLINDRICAL_SURFACE('',#6615,0.3);
#5298=CYLINDRICAL_SURFACE('',#6616,0.3);
#5299=CYLINDRICAL_SURFACE('',#6617,0.3);
#5300=CYLINDRICAL_SURFACE('',#6618,0.3);
#5301=CYLINDRICAL_SURFACE('',#6619,0.3);
#5302=CYLINDRICAL_SURFACE('',#6632,0.3);
#5303=CYLINDRICAL_SURFACE('',#6637,0.3);
#5304=CYLINDRICAL_SURFACE('',#6638,0.3);
#5305=CYLINDRICAL_SURFACE('',#6639,0.3);
#5306=CYLINDRICAL_SURFACE('',#6640,0.3);
#5307=CYLINDRICAL_SURFACE('',#6641,0.3);
#5308=CYLINDRICAL_SURFACE('',#6642,0.3);
#5309=CYLINDRICAL_SURFACE('',#6646,0.3);
#5310=CYLINDRICAL_SURFACE('',#6656,0.3);
#5311=CYLINDRICAL_SURFACE('',#6657,0.3);
#5312=CYLINDRICAL_SURFACE('',#6658,0.3);
#5313=CYLINDRICAL_SURFACE('',#6659,0.3);
#5314=CYLINDRICAL_SURFACE('',#6660,0.3);
#5315=CYLINDRICAL_SURFACE('',#6661,0.3);
#5316=CYLINDRICAL_SURFACE('',#6662,0.3);
#5317=CYLINDRICAL_SURFACE('',#6663,0.3);
#5318=CYLINDRICAL_SURFACE('',#6664,0.3);
#5319=CYLINDRICAL_SURFACE('',#6665,0.3);
#5320=CYLINDRICAL_SURFACE('',#6666,0.3);
#5321=CYLINDRICAL_SURFACE('',#6667,0.3);
#5322=CYLINDRICAL_SURFACE('',#6668,0.3);
#5323=CYLINDRICAL_SURFACE('',#6669,0.3);
#5324=CYLINDRICAL_SURFACE('',#6671,4.);
#5325=CYLINDRICAL_SURFACE('',#6672,4.);
#5619=ADVANCED_FACE('',(#676),#235,.T.);
#5620=ADVANCED_FACE('',(#677,#286,#287),#367,.T.);
#5621=ADVANCED_FACE('',(#678),#5280,.F.);
#5622=ADVANCED_FACE('',(#679),#236,.T.);
#5623=ADVANCED_FACE('',(#680),#5281,.F.);
#5624=ADVANCED_FACE('',(#681),#237,.T.);
#5625=ADVANCED_FACE('',(#682,#288,#289),#368,.F.);
#5626=ADVANCED_FACE('',(#683),#5282,.F.);
#5627=ADVANCED_FACE('',(#684),#238,.T.);
#5628=ADVANCED_FACE('',(#685),#5283,.F.);
#5629=ADVANCED_FACE('',(#686),#143,.T.);
#5630=ADVANCED_FACE('',(#687),#144,.T.);
#5631=ADVANCED_FACE('',(#688),#145,.T.);
#5632=ADVANCED_FACE('',(#689),#5284,.T.);
#5633=ADVANCED_FACE('',(#690),#146,.T.);
#5634=ADVANCED_FACE('',(#691),#5285,.T.);
#5635=ADVANCED_FACE('',(#692),#147,.T.);
#5636=ADVANCED_FACE('',(#693),#5286,.T.);
#5637=ADVANCED_FACE('',(#694),#5287,.T.);
#5638=ADVANCED_FACE('',(#695),#148,.T.);
#5639=ADVANCED_FACE('',(#696),#5288,.T.);
#5640=ADVANCED_FACE('',(#697),#149,.T.);
#5641=ADVANCED_FACE('',(#698),#239,.T.);
#5642=ADVANCED_FACE('',(#699),#150,.T.);
#5643=ADVANCED_FACE('',(#700),#5289,.T.);
#5644=ADVANCED_FACE('',(#701),#240,.T.);
#5645=ADVANCED_FACE('',(#702),#241,.T.);
#5646=ADVANCED_FACE('',(#703),#151,.T.);
#5647=ADVANCED_FACE('',(#704),#5290,.T.);
#5648=ADVANCED_FACE('',(#705),#242,.T.);
#5649=ADVANCED_FACE('',(#706),#152,.T.);
#5650=ADVANCED_FACE('',(#707),#5291,.T.);
#5651=ADVANCED_FACE('',(#708),#153,.T.);
#5652=ADVANCED_FACE('',(#709),#5292,.T.);
#5653=ADVANCED_FACE('',(#710),#154,.T.);
#5654=ADVANCED_FACE('',(#711),#5293,.T.);
#5655=ADVANCED_FACE('',(#712),#155,.T.);
#5656=ADVANCED_FACE('',(#713),#5294,.T.);
#5657=ADVANCED_FACE('',(#714),#5295,.T.);
#5658=ADVANCED_FACE('',(#715),#156,.T.);
#5659=ADVANCED_FACE('',(#716),#157,.T.);
#5660=ADVANCED_FACE('',(#717),#5296,.T.);
#5661=ADVANCED_FACE('',(#718),#158,.T.);
#5662=ADVANCED_FACE('',(#719),#5297,.T.);
#5663=ADVANCED_FACE('',(#720),#5298,.T.);
#5664=ADVANCED_FACE('',(#721),#5299,.T.);
#5665=ADVANCED_FACE('',(#722),#5300,.T.);
#5666=ADVANCED_FACE('',(#723),#5301,.T.);
#5667=ADVANCED_FACE('',(#724),#159,.T.);
#5668=ADVANCED_FACE('',(#725),#160,.T.);
#5669=ADVANCED_FACE('',(#726),#161,.T.);
#5670=ADVANCED_FACE('',(#727),#5302,.T.);
#5671=ADVANCED_FACE('',(#728),#162,.T.);
#5672=ADVANCED_FACE('',(#729),#5303,.T.);
#5673=ADVANCED_FACE('',(#730),#5304,.T.);
#5674=ADVANCED_FACE('',(#731),#5305,.T.);
#5675=ADVANCED_FACE('',(#732),#5306,.T.);
#5676=ADVANCED_FACE('',(#733),#5307,.T.);
#5677=ADVANCED_FACE('',(#734),#5308,.T.);
#5678=ADVANCED_FACE('',(#735),#243,.T.);
#5679=ADVANCED_FACE('',(#736),#5309,.T.);
#5680=ADVANCED_FACE('',(#737),#244,.T.);
#5681=ADVANCED_FACE('',(#738),#245,.T.);
#5682=ADVANCED_FACE('',(#739),#246,.T.);
#5683=ADVANCED_FACE('',(#740),#5310,.T.);
#5684=ADVANCED_FACE('',(#741),#5311,.T.);
#5685=ADVANCED_FACE('',(#742),#5312,.T.);
#5686=ADVANCED_FACE('',(#743),#5313,.T.);
#5687=ADVANCED_FACE('',(#744),#5314,.T.);
#5688=ADVANCED_FACE('',(#745),#5315,.F.);
#5689=ADVANCED_FACE('',(#746),#5316,.T.);
#5690=ADVANCED_FACE('',(#747),#5317,.F.);
#5691=ADVANCED_FACE('',(#748),#5318,.T.);
#5692=ADVANCED_FACE('',(#749),#5319,.T.);
#5693=ADVANCED_FACE('',(#750),#5320,.T.);
#5694=ADVANCED_FACE('',(#751),#5321,.T.);
#5695=ADVANCED_FACE('',(#752),#5322,.T.);
#5696=ADVANCED_FACE('',(#753),#5323,.T.);
#5697=ADVANCED_FACE('',(#754),#369,.T.);
#5698=ADVANCED_FACE('',(#755),#5324,.F.);
#5699=ADVANCED_FACE('',(#756),#5325,.F.);
#5700=ADVANCED_FACE('',(#757),#370,.F.);
#5701=ADVANCED_FACE('',(#758,#290,#291,#292,#293),#371,.T.);
#5702=ADVANCED_FACE('',(#759),#372,.T.);
#5703=ADVANCED_FACE('',(#760),#373,.F.);
#5704=ADVANCED_FACE('',(#761),#374,.T.);
#5705=ADVANCED_FACE('',(#762),#375,.T.);
#5706=ADVANCED_FACE('',(#763),#376,.T.);
#5707=ADVANCED_FACE('',(#764),#377,.T.);
#5708=ADVANCED_FACE('',(#765),#378,.T.);
#5709=ADVANCED_FACE('',(#766),#379,.T.);
#5710=ADVANCED_FACE('',(#767),#380,.T.);
#5711=ADVANCED_FACE('',(#768),#381,.T.);
#5712=ADVANCED_FACE('',(#769),#382,.F.);
#5722=CLOSED_SHELL('',(#5619,#5620,#5621,#5622,#5623,#5624,#5625,#5626,
#5627,#5628,#5629,#5630,#5631,#5632,#5633,#5634,#5635,#5636,#5637,#5638,
#5639,#5640,#5641,#5642,#5643,#5644,#5645,#5646,#5647,#5648,#5649,#5650,
#5651,#5652,#5653,#5654,#5655,#5656,#5657,#5658,#5659,#5660,#5661,#5662,
#5663,#5664,#5665,#5666,#5667,#5668,#5669,#5670,#5671,#5672,#5673,#5674,
#5675,#5676,#5677,#5678,#5679,#5680,#5681,#5682,#5683,#5684,#5685,#5686,
#5687,#5688,#5689,#5690,#5691,#5692,#5693,#5694,#5695,#5696,#5697,#5698,
#5699,#5700,#5701,#5702,#5703,#5704,#5705,#5706,#5707,#5708,#5709,#5710,
#5711,#5712));
#6489=AXIS2_PLACEMENT_3D('',#10103,#8248,#8249);
#6490=AXIS2_PLACEMENT_3D('',#10104,#8250,#8251);
#6491=AXIS2_PLACEMENT_3D('',#10106,#8252,#8253);
#6492=AXIS2_PLACEMENT_3D('',#10108,#8254,#8255);
#6493=AXIS2_PLACEMENT_3D('',#10109,#8256,#8257);
#6494=AXIS2_PLACEMENT_3D('',#10110,#8258,#8259);
#6495=AXIS2_PLACEMENT_3D('',#10120,#8264,#8265);
#6496=AXIS2_PLACEMENT_3D('',#10121,#8266,#8267);
#6497=AXIS2_PLACEMENT_3D('',#10124,#8269,#8270);
#6498=AXIS2_PLACEMENT_3D('',#10125,#8271,#8272);
#6499=AXIS2_PLACEMENT_3D('',#10127,#8273,#8274);
#6500=AXIS2_PLACEMENT_3D('',#10128,#8275,#8276);
#6501=AXIS2_PLACEMENT_3D('',#10129,#8277,#8278);
#6502=AXIS2_PLACEMENT_3D('',#10132,#8280,#8281);
#6503=AXIS2_PLACEMENT_3D('',#10133,#8282,#8283);
#6504=AXIS2_PLACEMENT_3D('',#10135,#8284,#8285);
#6505=AXIS2_PLACEMENT_3D('',#10137,#8286,#8287);
#6506=AXIS2_PLACEMENT_3D('',#10139,#8288,#8289);
#6507=AXIS2_PLACEMENT_3D('',#10140,#8290,#8291);
#6508=AXIS2_PLACEMENT_3D('',#10141,#8292,#8293);
#6509=AXIS2_PLACEMENT_3D('',#10151,#8298,#8299);
#6510=AXIS2_PLACEMENT_3D('',#10152,#8300,#8301);
#6511=AXIS2_PLACEMENT_3D('',#10155,#8303,#8304);
#6512=AXIS2_PLACEMENT_3D('',#10156,#8305,#8306);
#6513=AXIS2_PLACEMENT_3D('',#10158,#8307,#8308);
#6514=AXIS2_PLACEMENT_3D('',#10160,#8309,#8310);
#6515=AXIS2_PLACEMENT_3D('',#10161,#8311,#8312);
#6516=AXIS2_PLACEMENT_3D('',#10162,#8313,#8314);
#6517=AXIS2_PLACEMENT_3D('',#10165,#8316,#8317);
#6518=AXIS2_PLACEMENT_3D('',#10166,#8318,#8319);
#6519=AXIS2_PLACEMENT_3D('',#10169,#8320,#8321);
#6520=AXIS2_PLACEMENT_3D('',#10171,#8322,#8323);
#6521=AXIS2_PLACEMENT_3D('',#10172,#8324,#8325);
#6522=AXIS2_PLACEMENT_3D('',#10173,#8326,#8327);
#6523=AXIS2_PLACEMENT_3D('',#10176,#8328,#8329);
#6524=AXIS2_PLACEMENT_3D('',#10178,#8330,#8331);
#6525=AXIS2_PLACEMENT_3D('',#10179,#8332,#8333);
#6526=AXIS2_PLACEMENT_3D('',#10180,#8334,#8335);
#6527=AXIS2_PLACEMENT_3D('',#10183,#8336,#8337);
#6528=AXIS2_PLACEMENT_3D('',#10185,#8338,#8339);
#6529=AXIS2_PLACEMENT_3D('',#10186,#8340,#8341);
#6530=AXIS2_PLACEMENT_3D('',#10187,#8342,#8343);
#6531=AXIS2_PLACEMENT_3D('',#10190,#8346,#8347);
#6532=AXIS2_PLACEMENT_3D('',#10192,#8348,#8349);
#6533=AXIS2_PLACEMENT_3D('',#10194,#8350,#8351);
#6534=AXIS2_PLACEMENT_3D('',#10195,#8352,#8353);
#6535=AXIS2_PLACEMENT_3D('',#10196,#8354,#8355);
#6536=AXIS2_PLACEMENT_3D('',#10199,#8358,#8359);
#6537=AXIS2_PLACEMENT_3D('',#10202,#8360,#8361);
#6538=AXIS2_PLACEMENT_3D('',#10204,#8362,#8363);
#6539=AXIS2_PLACEMENT_3D('',#10205,#8364,#8365);
#6540=AXIS2_PLACEMENT_3D('',#10206,#8366,#8367);
#6541=AXIS2_PLACEMENT_3D('',#10209,#8370,#8371);
#6542=AXIS2_PLACEMENT_3D('',#10212,#8374,#8375);
#6543=AXIS2_PLACEMENT_3D('',#10214,#8376,#8377);
#6544=AXIS2_PLACEMENT_3D('',#10216,#8378,#8379);
#6545=AXIS2_PLACEMENT_3D('',#10217,#8380,#8381);
#6546=AXIS2_PLACEMENT_3D('',#10218,#8382,#8383);
#6547=AXIS2_PLACEMENT_3D('',#10221,#8386,#8387);
#6548=AXIS2_PLACEMENT_3D('',#10224,#8388,#8389);
#6549=AXIS2_PLACEMENT_3D('',#10225,#8390,#8391);
#6550=AXIS2_PLACEMENT_3D('',#10226,#8392,#8393);
#6551=AXIS2_PLACEMENT_3D('',#10227,#8394,#8395);
#6552=AXIS2_PLACEMENT_3D('',#10229,#8396,#8397);
#6553=AXIS2_PLACEMENT_3D('',#10231,#8398,#8399);
#6554=AXIS2_PLACEMENT_3D('',#10233,#8400,#8401);
#6555=AXIS2_PLACEMENT_3D('',#10234,#8402,#8403);
#6556=AXIS2_PLACEMENT_3D('',#10235,#8404,#8405);
#6557=AXIS2_PLACEMENT_3D('',#10238,#8406,#8407);
#6558=AXIS2_PLACEMENT_3D('',#10239,#8408,#8409);
#6559=AXIS2_PLACEMENT_3D('',#10240,#8410,#8411);
#6560=AXIS2_PLACEMENT_3D('',#10241,#8412,#8413);
#6561=AXIS2_PLACEMENT_3D('',#10243,#8415,#8416);
#6562=AXIS2_PLACEMENT_3D('',#10246,#8417,#8418);
#6563=AXIS2_PLACEMENT_3D('',#10248,#8419,#8420);
#6564=AXIS2_PLACEMENT_3D('',#10249,#8421,#8422);
#6565=AXIS2_PLACEMENT_3D('',#10250,#8423,#8424);
#6566=AXIS2_PLACEMENT_3D('',#10251,#8425,#8426);
#6567=AXIS2_PLACEMENT_3D('',#10254,#8427,#8428);
#6568=AXIS2_PLACEMENT_3D('',#10256,#8429,#8430);
#6569=AXIS2_PLACEMENT_3D('',#10257,#8431,#8432);
#6570=AXIS2_PLACEMENT_3D('',#10258,#8433,#8434);
#6571=AXIS2_PLACEMENT_3D('',#10259,#8435,#8436);
#6572=AXIS2_PLACEMENT_3D('',#10262,#8437,#8438);
#6573=AXIS2_PLACEMENT_3D('',#10264,#8439,#8440);
#6574=AXIS2_PLACEMENT_3D('',#10265,#8441,#8442);
#6575=AXIS2_PLACEMENT_3D('',#10266,#8443,#8444);
#6576=AXIS2_PLACEMENT_3D('',#10269,#8447,#8448);
#6577=AXIS2_PLACEMENT_3D('',#10271,#8449,#8450);
#6578=AXIS2_PLACEMENT_3D('',#10273,#8451,#8452);
#6579=AXIS2_PLACEMENT_3D('',#10275,#8453,#8454);
#6580=AXIS2_PLACEMENT_3D('',#10276,#8455,#8456);
#6581=AXIS2_PLACEMENT_3D('',#10277,#8457,#8458);
#6582=AXIS2_PLACEMENT_3D('',#10280,#8459,#8460);
#6583=AXIS2_PLACEMENT_3D('',#10282,#8461,#8462);
#6584=AXIS2_PLACEMENT_3D('',#10283,#8463,#8464);
#6585=AXIS2_PLACEMENT_3D('',#10284,#8465,#8466);
#6586=AXIS2_PLACEMENT_3D('',#10287,#8469,#8470);
#6587=AXIS2_PLACEMENT_3D('',#10290,#8471,#8472);
#6588=AXIS2_PLACEMENT_3D('',#10292,#8473,#8474);
#6589=AXIS2_PLACEMENT_3D('',#10293,#8475,#8476);
#6590=AXIS2_PLACEMENT_3D('',#10294,#8477,#8478);
#6591=AXIS2_PLACEMENT_3D('',#10297,#8481,#8482);
#6592=AXIS2_PLACEMENT_3D('',#10300,#8483,#8484);
#6593=AXIS2_PLACEMENT_3D('',#10302,#8485,#8486);
#6594=AXIS2_PLACEMENT_3D('',#10303,#8487,#8488);
#6595=AXIS2_PLACEMENT_3D('',#10304,#8489,#8490);
#6596=AXIS2_PLACEMENT_3D('',#10307,#8493,#8494);
#6597=AXIS2_PLACEMENT_3D('',#10310,#8495,#8496);
#6598=AXIS2_PLACEMENT_3D('',#10312,#8497,#8498);
#6599=AXIS2_PLACEMENT_3D('',#10313,#8499,#8500);
#6600=AXIS2_PLACEMENT_3D('',#10314,#8501,#8502);
#6601=AXIS2_PLACEMENT_3D('',#10317,#8505,#8506);
#6602=AXIS2_PLACEMENT_3D('',#10320,#8509,#8510);
#6603=AXIS2_PLACEMENT_3D('',#10323,#8511,#8512);
#6604=AXIS2_PLACEMENT_3D('',#10325,#8513,#8514);
#6605=AXIS2_PLACEMENT_3D('',#10326,#8515,#8516);
#6606=AXIS2_PLACEMENT_3D('',#10327,#8517,#8518);
#6607=AXIS2_PLACEMENT_3D('',#10330,#8519,#8520);
#6608=AXIS2_PLACEMENT_3D('',#10332,#8521,#8522);
#6609=AXIS2_PLACEMENT_3D('',#10333,#8523,#8524);
#6610=AXIS2_PLACEMENT_3D('',#10334,#8525,#8526);
#6611=AXIS2_PLACEMENT_3D('',#10353,#8529,#8530);
#6612=AXIS2_PLACEMENT_3D('',#10356,#8531,#8532);
#6613=AXIS2_PLACEMENT_3D('',#10358,#8533,#8534);
#6614=AXIS2_PLACEMENT_3D('',#10359,#8535,#8536);
#6615=AXIS2_PLACEMENT_3D('',#10360,#8537,#8538);
#6616=AXIS2_PLACEMENT_3D('',#10363,#8541,#8542);
#6617=AXIS2_PLACEMENT_3D('',#10366,#8545,#8546);
#6618=AXIS2_PLACEMENT_3D('',#10385,#8549,#8550);
#6619=AXIS2_PLACEMENT_3D('',#10404,#8553,#8554);
#6620=AXIS2_PLACEMENT_3D('',#10423,#8557,#8558);
#6621=AXIS2_PLACEMENT_3D('',#10426,#8559,#8560);
#6622=AXIS2_PLACEMENT_3D('',#10428,#8561,#8562);
#6623=AXIS2_PLACEMENT_3D('',#10429,#8563,#8564);
#6624=AXIS2_PLACEMENT_3D('',#10430,#8565,#8566);
#6625=AXIS2_PLACEMENT_3D('',#10433,#8567,#8568);
#6626=AXIS2_PLACEMENT_3D('',#10435,#8569,#8570);
#6627=AXIS2_PLACEMENT_3D('',#10436,#8571,#8572);
#6628=AXIS2_PLACEMENT_3D('',#10437,#8573,#8574);
#6629=AXIS2_PLACEMENT_3D('',#10440,#8575,#8576);
#6630=AXIS2_PLACEMENT_3D('',#10442,#8577,#8578);
#6631=AXIS2_PLACEMENT_3D('',#10443,#8579,#8580);
#6632=AXIS2_PLACEMENT_3D('',#10444,#8581,#8582);
#6633=AXIS2_PLACEMENT_3D('',#10447,#8585,#8586);
#6634=AXIS2_PLACEMENT_3D('',#10450,#8587,#8588);
#6635=AXIS2_PLACEMENT_3D('',#10452,#8589,#8590);
#6636=AXIS2_PLACEMENT_3D('',#10453,#8591,#8592);
#6637=AXIS2_PLACEMENT_3D('',#10454,#8593,#8594);
#6638=AXIS2_PLACEMENT_3D('',#10473,#8597,#8598);
#6639=AXIS2_PLACEMENT_3D('',#10476,#8601,#8602);
#6640=AXIS2_PLACEMENT_3D('',#10479,#8605,#8606);
#6641=AXIS2_PLACEMENT_3D('',#10498,#8609,#8610);
#6642=AXIS2_PLACEMENT_3D('',#10501,#8613,#8614);
#6643=AXIS2_PLACEMENT_3D('',#10520,#8617,#8618);
#6644=AXIS2_PLACEMENT_3D('',#10521,#8619,#8620);
#6645=AXIS2_PLACEMENT_3D('',#10522,#8621,#8622);
#6646=AXIS2_PLACEMENT_3D('',#10523,#8623,#8624);
#6647=AXIS2_PLACEMENT_3D('',#10542,#8627,#8628);
#6648=AXIS2_PLACEMENT_3D('',#10543,#8629,#8630);
#6649=AXIS2_PLACEMENT_3D('',#10544,#8631,#8632);
#6650=AXIS2_PLACEMENT_3D('',#10545,#8633,#8634);
#6651=AXIS2_PLACEMENT_3D('',#10546,#8635,#8636);
#6652=AXIS2_PLACEMENT_3D('',#10547,#8637,#8638);
#6653=AXIS2_PLACEMENT_3D('',#10548,#8639,#8640);
#6654=AXIS2_PLACEMENT_3D('',#10549,#8641,#8642);
#6655=AXIS2_PLACEMENT_3D('',#10550,#8643,#8644);
#6656=AXIS2_PLACEMENT_3D('',#10551,#8645,#8646);
#6657=AXIS2_PLACEMENT_3D('',#10554,#8649,#8650);
#6658=AXIS2_PLACEMENT_3D('',#10557,#8653,#8654);
#6659=AXIS2_PLACEMENT_3D('',#10560,#8657,#8658);
#6660=AXIS2_PLACEMENT_3D('',#10563,#8661,#8662);
#6661=AXIS2_PLACEMENT_3D('',#10565,#8664,#8665);
#6662=AXIS2_PLACEMENT_3D('',#10567,#8667,#8668);
#6663=AXIS2_PLACEMENT_3D('',#10569,#8670,#8671);
#6664=AXIS2_PLACEMENT_3D('',#10571,#8673,#8674);
#6665=AXIS2_PLACEMENT_3D('',#10573,#8676,#8677);
#6666=AXIS2_PLACEMENT_3D('',#10576,#8680,#8681);
#6667=AXIS2_PLACEMENT_3D('',#10578,#8683,#8684);
#6668=AXIS2_PLACEMENT_3D('',#10581,#8687,#8688);
#6669=AXIS2_PLACEMENT_3D('',#10583,#8690,#8691);
#6670=AXIS2_PLACEMENT_3D('',#10586,#8694,#8695);
#6671=AXIS2_PLACEMENT_3D('',#10588,#8697,#8698);
#6672=AXIS2_PLACEMENT_3D('',#10590,#8700,#8701);
#6673=AXIS2_PLACEMENT_3D('',#10593,#8704,#8705);
#6674=AXIS2_PLACEMENT_3D('',#10594,#8706,#8707);
#6675=AXIS2_PLACEMENT_3D('',#10595,#8708,#8709);
#6676=AXIS2_PLACEMENT_3D('',#10596,#8710,#8711);
#6677=AXIS2_PLACEMENT_3D('',#10597,#8712,#8713);
#6678=AXIS2_PLACEMENT_3D('',#10598,#8714,#8715);
#6679=AXIS2_PLACEMENT_3D('',#10599,#8716,#8717);
#6680=AXIS2_PLACEMENT_3D('',#10600,#8718,#8719);
#6681=AXIS2_PLACEMENT_3D('',#10601,#8720,#8721);
#6682=AXIS2_PLACEMENT_3D('',#10602,#8722,#8723);
#6683=AXIS2_PLACEMENT_3D('',#10603,#8724,#8725);
#6684=AXIS2_PLACEMENT_3D('',#10604,#8726,#8727);
#6685=AXIS2_PLACEMENT_3D('',#10605,#8728,#8729);
#8248=DIRECTION('axis',(0.,0.,1.));
#8249=DIRECTION('refdir',(1.,0.,0.));
#8250=DIRECTION('center_axis',(0.,0.,1.));
#8251=DIRECTION('ref_axis',(1.,0.,0.));
#8252=DIRECTION('center_axis',(0.,0.,-1.));
#8253=DIRECTION('ref_axis',(1.,0.,0.));
#8254=DIRECTION('center_axis',(0.,-1.,0.));
#8255=DIRECTION('ref_axis',(-1.,0.,0.));
#8256=DIRECTION('center_axis',(0.,0.,1.));
#8257=DIRECTION('ref_axis',(1.,0.,0.));
#8258=DIRECTION('center_axis',(0.,0.,1.));
#8259=DIRECTION('ref_axis',(1.,0.,0.));
#8260=DIRECTION('',(1.,0.,0.));
#8261=DIRECTION('',(-5.9211894646675E-16,1.,0.));
#8262=DIRECTION('',(-1.,-2.77555756156289E-16,0.));
#8263=DIRECTION('',(0.,-1.,0.));
#8264=DIRECTION('center_axis',(0.,0.,1.));
#8265=DIRECTION('ref_axis',(1.,0.,0.));
#8266=DIRECTION('center_axis',(0.,0.,-1.));
#8267=DIRECTION('ref_axis',(1.,0.,0.));
#8268=DIRECTION('',(0.,0.,-1.));
#8269=DIRECTION('center_axis',(0.,0.,-1.));
#8270=DIRECTION('ref_axis',(1.,0.,0.));
#8271=DIRECTION('center_axis',(0.,0.,1.));
#8272=DIRECTION('ref_axis',(1.,0.,0.));
#8273=DIRECTION('center_axis',(0.,0.,-1.));
#8274=DIRECTION('ref_axis',(1.,0.,0.));
#8275=DIRECTION('center_axis',(0.,-1.,0.));
#8276=DIRECTION('ref_axis',(-1.,0.,0.));
#8277=DIRECTION('center_axis',(0.,0.,-1.));
#8278=DIRECTION('ref_axis',(1.,0.,0.));
#8279=DIRECTION('',(0.,0.,-1.));
#8280=DIRECTION('center_axis',(0.,0.,-1.));
#8281=DIRECTION('ref_axis',(1.,0.,0.));
#8282=DIRECTION('center_axis',(0.,0.,-1.));
#8283=DIRECTION('ref_axis',(-1.,0.,0.));
#8284=DIRECTION('center_axis',(0.,0.,1.));
#8285=DIRECTION('ref_axis',(1.,0.,0.));
#8286=DIRECTION('center_axis',(0.,-1.,0.));
#8287=DIRECTION('ref_axis',(1.,0.,0.));
#8288=DIRECTION('center_axis',(0.,0.,-1.));
#8289=DIRECTION('ref_axis',(1.,0.,0.));
#8290=DIRECTION('center_axis',(0.,0.,-1.));
#8291=DIRECTION('ref_axis',(1.,0.,0.));
#8292=DIRECTION('center_axis',(0.,0.,-1.));
#8293=DIRECTION('ref_axis',(1.,0.,0.));
#8294=DIRECTION('',(1.,0.,0.));
#8295=DIRECTION('',(-5.9211894646675E-16,1.,0.));
#8296=DIRECTION('',(-1.,0.,0.));
#8297=DIRECTION('',(0.,-1.,0.));
#8298=DIRECTION('center_axis',(0.,0.,1.));
#8299=DIRECTION('ref_axis',(1.,0.,0.));
#8300=DIRECTION('center_axis',(0.,0.,1.));
#8301=DIRECTION('ref_axis',(1.,0.,0.));
#8302=DIRECTION('',(0.,0.,-1.));
#8303=DIRECTION('center_axis',(0.,0.,1.));
#8304=DIRECTION('ref_axis',(1.,0.,0.));
#8305=DIRECTION('center_axis',(0.,0.,-1.));
#8306=DIRECTION('ref_axis',(-1.,0.,0.));
#8307=DIRECTION('center_axis',(0.,-1.,0.));
#8308=DIRECTION('ref_axis',(1.,0.,0.));
#8309=DIRECTION('center_axis',(0.,0.,-1.));
#8310=DIRECTION('ref_axis',(1.,0.,0.));
#8311=DIRECTION('center_axis',(0.,0.,-1.));
#8312=DIRECTION('ref_axis',(1.,0.,0.));
#8313=DIRECTION('center_axis',(0.,0.,1.));
#8314=DIRECTION('ref_axis',(1.,0.,0.));
#8315=DIRECTION('',(0.,0.,-1.));
#8316=DIRECTION('center_axis',(0.,0.,1.));
#8317=DIRECTION('ref_axis',(1.,0.,0.));
#8318=DIRECTION('center_axis',(0.408248290463861,0.408248290463837,-0.81649658092774));
#8319=DIRECTION('ref_axis',(-0.577350269189669,-0.577350269189598,-0.57735026918961));
#8320=DIRECTION('center_axis',(0.,-7.40148683083442E-15,-1.));
#8321=DIRECTION('ref_axis',(-1.,0.,0.));
#8322=DIRECTION('center_axis',(0.,-1.,0.));
#8323=DIRECTION('ref_axis',(0.,0.,-1.));
#8324=DIRECTION('center_axis',(-1.,0.,-5.92118946466745E-14));
#8325=DIRECTION('ref_axis',(0.,-1.,0.));
#8326=DIRECTION('center_axis',(-0.408248290463865,-0.81649658092773,0.408248290463853));
#8327=DIRECTION('ref_axis',(0.577350269189602,-0.577350269189626,-0.577350269189649));
#8328=DIRECTION('center_axis',(1.,0.,0.));
#8329=DIRECTION('ref_axis',(0.,0.,-1.));
#8330=DIRECTION('center_axis',(0.,-1.,-2.96059473233375E-14));
#8331=DIRECTION('ref_axis',(1.,0.,0.));
#8332=DIRECTION('center_axis',(-7.40148683083454E-15,0.,-1.));
#8333=DIRECTION('ref_axis',(0.,-1.,0.));
#8334=DIRECTION('center_axis',(-0.816496580927716,-0.408248290463882,0.408248290463864));
#8335=DIRECTION('ref_axis',(-0.577350269189634,0.577350269189634,-0.57735026918961));
#8336=DIRECTION('center_axis',(-1.,0.,0.));
#8337=DIRECTION('ref_axis',(0.,0.,-1.));
#8338=DIRECTION('center_axis',(0.,1.,0.));
#8339=DIRECTION('ref_axis',(-1.,0.,0.));
#8340=DIRECTION('center_axis',(0.,0.,-1.));
#8341=DIRECTION('ref_axis',(0.,1.,0.));
#8342=DIRECTION('center_axis',(-5.9211894646675E-16,1.,0.));
#8343=DIRECTION('ref_axis',(-0.707106781186563,0.,-0.707106781186532));
#8344=DIRECTION('',(5.9211894646675E-16,-1.,0.));
#8345=DIRECTION('',(-5.9211894646675E-16,1.,0.));
#8346=DIRECTION('center_axis',(-0.816496580927728,0.408248290463864,-0.408248290463858));
#8347=DIRECTION('ref_axis',(-0.577350269189594,-0.577350269189642,0.577350269189642));
#8348=DIRECTION('center_axis',(0.,-1.,0.));
#8349=DIRECTION('ref_axis',(-1.,0.,0.));
#8350=DIRECTION('center_axis',(-7.40148683083454E-15,0.,1.));
#8351=DIRECTION('ref_axis',(0.,-1.,0.));
#8352=DIRECTION('center_axis',(-1.,0.,0.));
#8353=DIRECTION('ref_axis',(0.,0.,1.));
#8354=DIRECTION('center_axis',(0.,0.,1.));
#8355=DIRECTION('ref_axis',(-0.707106781186516,-0.707106781186579,0.));
#8356=DIRECTION('',(0.,0.,-1.));
#8357=DIRECTION('',(0.,0.,1.));
#8358=DIRECTION('center_axis',(0.408248290463855,-0.816496580927734,-0.408248290463855));
#8359=DIRECTION('ref_axis',(0.577350269189651,0.577350269189604,-0.577350269189622));
#8360=DIRECTION('center_axis',(0.,0.,-1.));
#8361=DIRECTION('ref_axis',(1.,0.,0.));
#8362=DIRECTION('center_axis',(0.,1.,0.));
#8363=DIRECTION('ref_axis',(0.,0.,-1.));
#8364=DIRECTION('center_axis',(1.,0.,0.));
#8365=DIRECTION('ref_axis',(0.,1.,0.));
#8366=DIRECTION('center_axis',(0.,1.,0.));
#8367=DIRECTION('ref_axis',(0.707106781186563,0.,-0.707106781186532));
#8368=DIRECTION('',(0.,-1.,0.));
#8369=DIRECTION('',(0.,1.,0.));
#8370=DIRECTION('center_axis',(-1.,0.,0.));
#8371=DIRECTION('ref_axis',(0.,0.707106781186553,-0.707106781186542));
#8372=DIRECTION('',(1.,0.,0.));
#8373=DIRECTION('',(-1.,0.,0.));
#8374=DIRECTION('center_axis',(-0.408248290463864,-0.816496580927728,-0.408248290463858));
#8375=DIRECTION('ref_axis',(0.5773502691896,-0.577350269189624,0.577350269189653));
#8376=DIRECTION('center_axis',(1.,0.,0.));
#8377=DIRECTION('ref_axis',(0.,-1.,0.));
#8378=DIRECTION('center_axis',(0.,7.40148683083454E-15,1.));
#8379=DIRECTION('ref_axis',(1.,0.,0.));
#8380=DIRECTION('center_axis',(-1.48029736616691E-14,-1.,0.));
#8381=DIRECTION('ref_axis',(0.,0.,1.));
#8382=DIRECTION('center_axis',(0.,0.,1.));
#8383=DIRECTION('ref_axis',(0.707106781186568,-0.707106781186527,0.));
#8384=DIRECTION('',(0.,0.,-1.));
#8385=DIRECTION('',(0.,0.,1.));
#8386=DIRECTION('center_axis',(-0.408248290463856,-0.816496580927712,0.408248290463898));
#8387=DIRECTION('ref_axis',(-0.577350269189574,0.577350269189645,0.577350269189657));
#8388=DIRECTION('center_axis',(0.,0.,1.));
#8389=DIRECTION('ref_axis',(-1.,0.,0.));
#8390=DIRECTION('center_axis',(-1.48029736616699E-14,1.,0.));
#8391=DIRECTION('ref_axis',(0.,0.,1.));
#8392=DIRECTION('center_axis',(-1.,0.,-5.9211894646675E-14));
#8393=DIRECTION('ref_axis',(0.,1.,0.));
#8394=DIRECTION('center_axis',(1.,0.,0.));
#8395=DIRECTION('ref_axis',(0.,0.,-1.));
#8396=DIRECTION('center_axis',(1.,0.,0.));
#8397=DIRECTION('ref_axis',(0.,1.,0.));
#8398=DIRECTION('center_axis',(0.,0.,1.));
#8399=DIRECTION('ref_axis',(-1.,0.,0.));
#8400=DIRECTION('center_axis',(-1.,-5.9211894646675E-16,0.));
#8401=DIRECTION('ref_axis',(0.,0.707106781186545,-0.70710678118655));
#8402=DIRECTION('center_axis',(0.,-1.,0.));
#8403=DIRECTION('ref_axis',(0.,0.,1.));
#8404=DIRECTION('center_axis',(0.408248290463862,-0.816496580927724,0.408248290463868));
#8405=DIRECTION('ref_axis',(0.57735026918959,0.577350269189638,0.577350269189649));
#8406=DIRECTION('center_axis',(0.,0.,1.));
#8407=DIRECTION('ref_axis',(0.,1.,0.));
#8408=DIRECTION('center_axis',(1.,0.,0.));
#8409=DIRECTION('ref_axis',(0.,0.,1.));
#8410=DIRECTION('center_axis',(0.,1.,0.));
#8411=DIRECTION('ref_axis',(1.,0.,0.));
#8412=DIRECTION('center_axis',(1.,0.,0.));
#8413=DIRECTION('ref_axis',(0.,0.707106781186542,0.707106781186553));
#8414=DIRECTION('',(-1.,0.,0.));
#8415=DIRECTION('center_axis',(1.,0.,0.));
#8416=DIRECTION('ref_axis',(0.,0.,-1.));
#8417=DIRECTION('center_axis',(1.,0.,0.));
#8418=DIRECTION('ref_axis',(0.,0.707106781186545,-0.70710678118655));
#8419=DIRECTION('center_axis',(0.,0.,1.));
#8420=DIRECTION('ref_axis',(0.,-1.,0.));
#8421=DIRECTION('center_axis',(-1.,0.,0.));
#8422=DIRECTION('ref_axis',(0.,0.,-1.));
#8423=DIRECTION('center_axis',(0.,-1.,0.));
#8424=DIRECTION('ref_axis',(1.,0.,0.));
#8425=DIRECTION('center_axis',(-1.,0.,0.));
#8426=DIRECTION('ref_axis',(0.,0.,1.));
#8427=DIRECTION('center_axis',(-1.,-5.9211894646675E-16,0.));
#8428=DIRECTION('ref_axis',(0.,-0.70710678118654,-0.707106781186555));
#8429=DIRECTION('center_axis',(0.,0.,1.));
#8430=DIRECTION('ref_axis',(0.,1.,0.));
#8431=DIRECTION('center_axis',(1.,5.92118946466763E-14,0.));
#8432=DIRECTION('ref_axis',(0.,0.,-1.));
#8433=DIRECTION('center_axis',(0.,1.,0.));
#8434=DIRECTION('ref_axis',(-1.,0.,0.));
#8435=DIRECTION('center_axis',(0.408248290463862,-0.816496580927724,-0.408248290463868));
#8436=DIRECTION('ref_axis',(-0.577350269189592,-0.577350269189639,0.577350269189645));
#8437=DIRECTION('center_axis',(0.,-1.,0.));
#8438=DIRECTION('ref_axis',(-1.,0.,0.));
#8439=DIRECTION('center_axis',(0.,0.,1.));
#8440=DIRECTION('ref_axis',(0.,-1.,0.));
#8441=DIRECTION('center_axis',(-1.,5.92118946466754E-14,0.));
#8442=DIRECTION('ref_axis',(0.,0.,1.));
#8443=DIRECTION('center_axis',(0.,0.,-1.));
#8444=DIRECTION('ref_axis',(-0.707106781186527,-0.707106781186568,0.));
#8445=DIRECTION('',(0.,0.,1.));
#8446=DIRECTION('',(0.,0.,-1.));
#8447=DIRECTION('center_axis',(-1.,0.,0.));
#8448=DIRECTION('ref_axis',(0.,0.,1.));
#8449=DIRECTION('center_axis',(-1.,0.,0.));
#8450=DIRECTION('ref_axis',(0.,-1.,0.));
#8451=DIRECTION('center_axis',(0.,0.,1.));
#8452=DIRECTION('ref_axis',(1.,0.,0.));
#8453=DIRECTION('center_axis',(1.,0.,0.));
#8454=DIRECTION('ref_axis',(0.,-0.70710678118654,-0.707106781186555));
#8455=DIRECTION('center_axis',(0.,1.,0.));
#8456=DIRECTION('ref_axis',(0.,0.,1.));
#8457=DIRECTION('center_axis',(-0.408248290463867,-0.816496580927722,-0.408248290463867));
#8458=DIRECTION('ref_axis',(0.5773502691896,-0.577350269189636,0.577350269189642));
#8459=DIRECTION('center_axis',(1.,0.,0.));
#8460=DIRECTION('ref_axis',(0.,-1.,0.));
#8461=DIRECTION('center_axis',(0.,0.,1.));
#8462=DIRECTION('ref_axis',(1.,0.,0.));
#8463=DIRECTION('center_axis',(0.,-1.,0.));
#8464=DIRECTION('ref_axis',(0.,0.,1.));
#8465=DIRECTION('center_axis',(0.,0.,1.));
#8466=DIRECTION('ref_axis',(0.707106781186568,-0.707106781186527,0.));
#8467=DIRECTION('',(0.,0.,-1.));
#8468=DIRECTION('',(0.,0.,1.));
#8469=DIRECTION('center_axis',(-0.408248290463866,-0.81649658092772,0.408248290463872));
#8470=DIRECTION('ref_axis',(-0.577350269189592,0.577350269189628,0.577350269189657));
#8471=DIRECTION('center_axis',(-1.,0.,5.9211894646675E-14));
#8472=DIRECTION('ref_axis',(0.,1.,0.));
#8473=DIRECTION('center_axis',(0.,0.,1.));
#8474=DIRECTION('ref_axis',(-1.,0.,0.));
#8475=DIRECTION('center_axis',(1.48029736616682E-14,1.,0.));
#8476=DIRECTION('ref_axis',(0.,0.,1.));
#8477=DIRECTION('center_axis',(0.,0.,1.));
#8478=DIRECTION('ref_axis',(-0.707106781186527,0.707106781186568,0.));
#8479=DIRECTION('',(0.,0.,-1.));
#8480=DIRECTION('',(0.,0.,1.));
#8481=DIRECTION('center_axis',(-0.408248290463859,0.408248290463847,-0.816496580927736));
#8482=DIRECTION('ref_axis',(-0.577350269189657,0.577350269189622,0.577350269189598));
#8483=DIRECTION('center_axis',(0.,7.40148683083442E-15,1.));
#8484=DIRECTION('ref_axis',(-1.,0.,0.));
#8485=DIRECTION('center_axis',(0.,1.,0.));
#8486=DIRECTION('ref_axis',(0.,0.,1.));
#8487=DIRECTION('center_axis',(-1.,0.,0.));
#8488=DIRECTION('ref_axis',(0.,1.,0.));
#8489=DIRECTION('center_axis',(5.9211894646675E-16,-1.,0.));
#8490=DIRECTION('ref_axis',(-0.707106781186563,0.,0.707106781186532));
#8491=DIRECTION('',(-5.9211894646675E-16,1.,0.));
#8492=DIRECTION('',(5.9211894646675E-16,-1.,0.));
#8493=DIRECTION('center_axis',(0.408248290463865,-0.81649658092773,0.408248290463853));
#8494=DIRECTION('ref_axis',(0.5773502691896,0.577350269189624,0.577350269189653));
#8495=DIRECTION('center_axis',(0.,1.,2.96059473233375E-14));
#8496=DIRECTION('ref_axis',(1.,0.,0.));
#8497=DIRECTION('center_axis',(0.,0.,1.));
#8498=DIRECTION('ref_axis',(0.,1.,0.));
#8499=DIRECTION('center_axis',(1.,0.,0.));
#8500=DIRECTION('ref_axis',(0.,0.,1.));
#8501=DIRECTION('center_axis',(0.,0.,1.));
#8502=DIRECTION('ref_axis',(0.707106781186568,0.707106781186527,0.));
#8503=DIRECTION('',(0.,0.,-1.));
#8504=DIRECTION('',(0.,0.,1.));
#8505=DIRECTION('center_axis',(-1.,-2.77555756156289E-16,0.));
#8506=DIRECTION('ref_axis',(0.,0.707106781186553,0.707106781186542));
#8507=DIRECTION('',(1.,2.77555756156289E-16,0.));
#8508=DIRECTION('',(-1.,-2.77555756156289E-16,0.));
#8509=DIRECTION('center_axis',(0.408248290463862,-0.816496580927724,0.408248290463868));
#8510=DIRECTION('ref_axis',(0.57735026918959,0.577350269189638,0.577350269189649));
#8511=DIRECTION('center_axis',(0.,1.,0.));
#8512=DIRECTION('ref_axis',(1.,0.,0.));
#8513=DIRECTION('center_axis',(-7.40148683083454E-15,0.,1.));
#8514=DIRECTION('ref_axis',(0.,1.,0.));
#8515=DIRECTION('center_axis',(1.,0.,0.));
#8516=DIRECTION('ref_axis',(0.,0.,1.));
#8517=DIRECTION('center_axis',(-0.408248290463859,-0.408248290463835,-0.816496580927742));
#8518=DIRECTION('ref_axis',(-0.577350269189663,-0.577350269189604,0.57735026918961));
#8519=DIRECTION('center_axis',(7.40148683083454E-15,0.,1.));
#8520=DIRECTION('ref_axis',(0.,-1.,0.));
#8521=DIRECTION('center_axis',(-1.,5.92118946466754E-14,0.));
#8522=DIRECTION('ref_axis',(0.,0.,1.));
#8523=DIRECTION('center_axis',(0.,-1.,0.));
#8524=DIRECTION('ref_axis',(-1.,0.,0.));
#8525=DIRECTION('center_axis',(0.,0.,-1.));
#8526=DIRECTION('ref_axis',(-0.707106781186516,0.707106781186579,0.));
#8527=DIRECTION('',(0.,0.,1.));
#8528=DIRECTION('',(0.,0.,-1.));
#8529=DIRECTION('center_axis',(-0.816496580927732,-0.408248290463866,0.408248290463848));
#8530=DIRECTION('ref_axis',(0.577350269189588,-0.577350269189659,0.57735026918963));
#8531=DIRECTION('center_axis',(0.,-7.40148683083454E-15,1.));
#8532=DIRECTION('ref_axis',(1.,0.,0.));
#8533=DIRECTION('center_axis',(-2.96059473233381E-14,-1.,0.));
#8534=DIRECTION('ref_axis',(0.,0.,1.));
#8535=DIRECTION('center_axis',(1.,0.,0.));
#8536=DIRECTION('ref_axis',(0.,-1.,0.));
#8537=DIRECTION('center_axis',(0.,1.,0.));
#8538=DIRECTION('ref_axis',(0.707106781186563,0.,0.707106781186532));
#8539=DIRECTION('',(0.,-1.,0.));
#8540=DIRECTION('',(0.,1.,0.));
#8541=DIRECTION('center_axis',(1.,0.,0.));
#8542=DIRECTION('ref_axis',(0.,-0.707106781186547,0.707106781186547));
#8543=DIRECTION('',(-1.,0.,0.));
#8544=DIRECTION('',(1.,0.,0.));
#8545=DIRECTION('center_axis',(0.,0.,1.));
#8546=DIRECTION('ref_axis',(0.707106781186558,0.707106781186537,0.));
#8547=DIRECTION('',(0.,0.,1.));
#8548=DIRECTION('',(0.,0.,-1.));
#8549=DIRECTION('center_axis',(0.,0.,1.));
#8550=DIRECTION('ref_axis',(-0.707106781186516,-0.707106781186579,0.));
#8551=DIRECTION('',(0.,0.,1.));
#8552=DIRECTION('',(0.,0.,-1.));
#8553=DIRECTION('center_axis',(0.,0.,-1.));
#8554=DIRECTION('ref_axis',(0.707106781186568,-0.707106781186527,0.));
#8555=DIRECTION('',(0.,0.,1.));
#8556=DIRECTION('',(0.,0.,-1.));
#8557=DIRECTION('center_axis',(-0.816496580927728,0.408248290463864,-0.408248290463858));
#8558=DIRECTION('ref_axis',(-0.577350269189588,-0.577350269189647,0.577350269189642));
#8559=DIRECTION('center_axis',(0.,0.,1.));
#8560=DIRECTION('ref_axis',(0.,-1.,0.));
#8561=DIRECTION('center_axis',(-1.,0.,0.));
#8562=DIRECTION('ref_axis',(0.,0.,1.));
#8563=DIRECTION('center_axis',(0.,-1.,0.));
#8564=DIRECTION('ref_axis',(-1.,0.,0.));
#8565=DIRECTION('center_axis',(-0.408248290463857,-0.816496580927726,-0.408248290463869));
#8566=DIRECTION('ref_axis',(0.57735026918959,-0.577350269189638,0.577350269189649));
#8567=DIRECTION('center_axis',(0.,0.,1.));
#8568=DIRECTION('ref_axis',(1.,0.,0.));
#8569=DIRECTION('center_axis',(0.,-1.,0.));
#8570=DIRECTION('ref_axis',(0.,0.,1.));
#8571=DIRECTION('center_axis',(1.,0.,0.));
#8572=DIRECTION('ref_axis',(0.,-1.,0.));
#8573=DIRECTION('center_axis',(-0.408248290463861,0.408248290463837,-0.81649658092774));
#8574=DIRECTION('ref_axis',(-0.577350269189665,0.577350269189606,0.577350269189606));
#8575=DIRECTION('center_axis',(0.,0.,1.));
#8576=DIRECTION('ref_axis',(-1.,0.,0.));
#8577=DIRECTION('center_axis',(0.,1.,0.));
#8578=DIRECTION('ref_axis',(0.,0.,1.));
#8579=DIRECTION('center_axis',(-1.,0.,5.9211894646675E-14));
#8580=DIRECTION('ref_axis',(0.,1.,0.));
#8581=DIRECTION('center_axis',(5.9211894646675E-16,-1.,0.));
#8582=DIRECTION('ref_axis',(-0.707106781186563,0.,0.707106781186532));
#8583=DIRECTION('',(-5.9211894646675E-16,1.,0.));
#8584=DIRECTION('',(5.9211894646675E-16,-1.,0.));
#8585=DIRECTION('center_axis',(0.408248290463868,-0.816496580927724,0.408248290463862));
#8586=DIRECTION('ref_axis',(0.577350269189598,0.577350269189634,0.577350269189645));
#8587=DIRECTION('center_axis',(0.,1.,0.));
#8588=DIRECTION('ref_axis',(1.,0.,0.));
#8589=DIRECTION('center_axis',(0.,0.,1.));
#8590=DIRECTION('ref_axis',(0.,1.,0.));
#8591=DIRECTION('center_axis',(1.,0.,0.));
#8592=DIRECTION('ref_axis',(0.,0.,1.));
#8593=DIRECTION('center_axis',(0.,0.,1.));
#8594=DIRECTION('ref_axis',(0.707106781186568,0.707106781186527,0.));
#8595=DIRECTION('',(0.,0.,1.));
#8596=DIRECTION('',(0.,0.,-1.));
#8597=DIRECTION('center_axis',(-1.,0.,0.));
#8598=DIRECTION('ref_axis',(0.,0.707106781186553,0.707106781186542));
#8599=DIRECTION('',(1.,0.,0.));
#8600=DIRECTION('',(-1.,0.,0.));
#8601=DIRECTION('center_axis',(0.,1.,0.));
#8602=DIRECTION('ref_axis',(0.707106781186563,0.,0.707106781186532));
#8603=DIRECTION('',(0.,-1.,0.));
#8604=DIRECTION('',(0.,1.,0.));
#8605=DIRECTION('center_axis',(0.,0.,-1.));
#8606=DIRECTION('ref_axis',(-0.707106781186516,0.707106781186579,0.));
#8607=DIRECTION('',(0.,0.,1.));
#8608=DIRECTION('',(0.,0.,-1.));
#8609=DIRECTION('center_axis',(1.,0.,0.));
#8610=DIRECTION('ref_axis',(0.,-0.707106781186553,0.707106781186542));
#8611=DIRECTION('',(-1.,0.,0.));
#8612=DIRECTION('',(1.,0.,0.));
#8613=DIRECTION('center_axis',(0.,0.,-1.));
#8614=DIRECTION('ref_axis',(0.707106781186558,-0.707106781186537,0.));
#8615=DIRECTION('',(0.,0.,1.));
#8616=DIRECTION('',(0.,0.,-1.));
#8617=DIRECTION('center_axis',(-1.,0.,0.));
#8618=DIRECTION('ref_axis',(0.,0.,-1.));
#8619=DIRECTION('center_axis',(-1.,0.,0.));
#8620=DIRECTION('ref_axis',(0.,0.,-1.));
#8621=DIRECTION('center_axis',(1.,0.,0.));
#8622=DIRECTION('ref_axis',(0.,0.,-1.));
#8623=DIRECTION('center_axis',(0.,0.,1.));
#8624=DIRECTION('ref_axis',(-0.707106781186516,-0.707106781186579,0.));
#8625=DIRECTION('',(0.,0.,1.));
#8626=DIRECTION('',(0.,0.,-1.));
#8627=DIRECTION('center_axis',(1.,5.9211894646675E-16,0.));
#8628=DIRECTION('ref_axis',(0.,0.,-1.));
#8629=DIRECTION('center_axis',(-1.,-5.9211894646675E-16,0.));
#8630=DIRECTION('ref_axis',(-2.62953635073665E-32,4.44089209850053E-17,
-1.));
#8631=DIRECTION('center_axis',(1.,5.9211894646675E-16,0.));
#8632=DIRECTION('ref_axis',(0.,4.44089209850053E-17,-1.));
#8633=DIRECTION('center_axis',(-1.,0.,0.));
#8634=DIRECTION('ref_axis',(0.,0.,-1.));
#8635=DIRECTION('center_axis',(1.,0.,0.));
#8636=DIRECTION('ref_axis',(0.,0.,-1.));
#8637=DIRECTION('center_axis',(-1.,0.,0.));
#8638=DIRECTION('ref_axis',(0.,0.,-1.));
#8639=DIRECTION('center_axis',(1.,5.9211894646675E-16,0.));
#8640=DIRECTION('ref_axis',(0.,0.,-1.));
#8641=DIRECTION('center_axis',(1.,5.9211894646675E-16,0.));
#8642=DIRECTION('ref_axis',(0.,4.44089209850053E-17,-1.));
#8643=DIRECTION('center_axis',(-1.,-5.9211894646675E-16,0.));
#8644=DIRECTION('ref_axis',(-2.62953635073665E-32,4.44089209850053E-17,
-1.));
#8645=DIRECTION('center_axis',(5.9211894646675E-16,-1.,0.));
#8646=DIRECTION('ref_axis',(-0.707106781186563,0.,0.707106781186532));
#8647=DIRECTION('',(-5.9211894646675E-16,1.,0.));
#8648=DIRECTION('',(5.9211894646675E-16,-1.,0.));
#8649=DIRECTION('center_axis',(-1.,0.,0.));
#8650=DIRECTION('ref_axis',(0.,0.707106781186547,0.707106781186547));
#8651=DIRECTION('',(1.,0.,0.));
#8652=DIRECTION('',(-1.,0.,0.));
#8653=DIRECTION('center_axis',(0.,1.,0.));
#8654=DIRECTION('ref_axis',(0.707106781186563,0.,0.707106781186532));
#8655=DIRECTION('',(0.,-1.,0.));
#8656=DIRECTION('',(0.,1.,0.));
#8657=DIRECTION('center_axis',(1.,0.,0.));
#8658=DIRECTION('ref_axis',(0.,-0.707106781186542,0.707106781186553));
#8659=DIRECTION('',(-1.,0.,0.));
#8660=DIRECTION('',(1.,0.,0.));
#8661=DIRECTION('center_axis',(0.,-1.,0.));
#8662=DIRECTION('ref_axis',(0.707106781186563,0.,0.707106781186532));
#8663=DIRECTION('',(0.,1.,0.));
#8664=DIRECTION('center_axis',(-1.,-2.77555756156289E-16,0.));
#8665=DIRECTION('ref_axis',(0.,-0.70710678118654,-0.707106781186555));
#8666=DIRECTION('',(1.,2.77555756156289E-16,0.));
#8667=DIRECTION('center_axis',(-5.9211894646675E-16,1.,0.));
#8668=DIRECTION('ref_axis',(-0.707106781186521,0.,0.707106781186574));
#8669=DIRECTION('',(5.9211894646675E-16,-1.,0.));
#8670=DIRECTION('center_axis',(1.,0.,0.));
#8671=DIRECTION('ref_axis',(0.,0.70710678118654,-0.707106781186555));
#8672=DIRECTION('',(-1.,0.,0.));
#8673=DIRECTION('center_axis',(0.,1.,0.));
#8674=DIRECTION('ref_axis',(0.707106781186563,0.,0.707106781186532));
#8675=DIRECTION('',(0.,1.,0.));
#8676=DIRECTION('center_axis',(0.,0.,1.));
#8677=DIRECTION('ref_axis',(0.707106781186568,0.707106781186527,0.));
#8678=DIRECTION('',(0.,0.,-1.));
#8679=DIRECTION('',(0.,0.,1.));
#8680=DIRECTION('center_axis',(5.9211894646675E-16,-1.,0.));
#8681=DIRECTION('ref_axis',(-0.707106781186563,0.,0.707106781186532));
#8682=DIRECTION('',(5.9211894646675E-16,-1.,0.));
#8683=DIRECTION('center_axis',(0.,0.,1.));
#8684=DIRECTION('ref_axis',(-0.707106781186516,0.707106781186579,0.));
#8685=DIRECTION('',(0.,0.,-1.));
#8686=DIRECTION('',(0.,0.,1.));
#8687=DIRECTION('center_axis',(1.,0.,0.));
#8688=DIRECTION('ref_axis',(0.,-0.707106781186553,0.707106781186542));
#8689=DIRECTION('',(1.,0.,0.));
#8690=DIRECTION('center_axis',(-1.,0.,0.));
#8691=DIRECTION('ref_axis',(0.,-0.707106781186547,-0.707106781186547));
#8692=DIRECTION('',(1.,0.,0.));
#8693=DIRECTION('',(-1.,0.,0.));
#8694=DIRECTION('center_axis',(0.,1.,0.));
#8695=DIRECTION('ref_axis',(0.,0.,1.));
#8696=DIRECTION('',(1.,0.,0.));
#8697=DIRECTION('center_axis',(-1.,0.,0.));
#8698=DIRECTION('ref_axis',(0.,6.12323399573677E-17,-1.));
#8699=DIRECTION('',(1.,0.,0.));
#8700=DIRECTION('center_axis',(1.,0.,0.));
#8701=DIRECTION('ref_axis',(0.,-6.12323399573677E-17,-1.));
#8702=DIRECTION('',(1.,0.,0.));
#8703=DIRECTION('',(1.,0.,0.));
#8704=DIRECTION('center_axis',(0.,1.,0.));
#8705=DIRECTION('ref_axis',(0.,0.,1.));
#8706=DIRECTION('center_axis',(0.,0.,-1.));
#8707=DIRECTION('ref_axis',(-1.,0.,0.));
#8708=DIRECTION('center_axis',(0.,-1.,0.));
#8709=DIRECTION('ref_axis',(1.,0.,0.));
#8710=DIRECTION('center_axis',(0.,-1.,0.));
#8711=DIRECTION('ref_axis',(1.,0.,0.));
#8712=DIRECTION('center_axis',(0.,-1.,0.));
#8713=DIRECTION('ref_axis',(1.,0.,0.));
#8714=DIRECTION('center_axis',(0.,0.,1.));
#8715=DIRECTION('ref_axis',(1.,0.,0.));
#8716=DIRECTION('center_axis',(-2.77555756156289E-16,1.,0.));
#8717=DIRECTION('ref_axis',(-1.,-2.77555756156289E-16,0.));
#8718=DIRECTION('center_axis',(0.,0.,1.));
#8719=DIRECTION('ref_axis',(1.,0.,0.));
#8720=DIRECTION('center_axis',(-1.,-5.9211894646675E-16,0.));
#8721=DIRECTION('ref_axis',(5.9211894646675E-16,-1.,0.));
#8722=DIRECTION('center_axis',(0.,0.,1.));
#8723=DIRECTION('ref_axis',(1.,0.,0.));
#8724=DIRECTION('center_axis',(1.,0.,0.));
#8725=DIRECTION('ref_axis',(0.,1.,0.));
#8726=DIRECTION('center_axis',(0.,-1.,0.));
#8727=DIRECTION('ref_axis',(0.,0.,-1.));
#8728=DIRECTION('center_axis',(0.,-1.,0.));
#8729=DIRECTION('ref_axis',(0.,0.,-1.));
#10103=CARTESIAN_POINT('',(0.,0.,0.));
#10104=CARTESIAN_POINT('Origin',(-133.037195913696,35.,-10.3));
#10105=CARTESIAN_POINT('',(-135.037195913696,35.,-10.3));
#10106=CARTESIAN_POINT('Origin',(-133.037195913696,35.,-10.3));
#10107=CARTESIAN_POINT('',(-135.337195913696,35.,-10.));
#10108=CARTESIAN_POINT('Origin',(-135.337195913696,35.,-10.3));
#10109=CARTESIAN_POINT('Origin',(-133.037195913696,35.,-10.));
#10110=CARTESIAN_POINT('Origin',(-137.,35.,-10.));
#10111=CARTESIAN_POINT('',(-144.7,39.7,-10.));
#10112=CARTESIAN_POINT('',(-129.3,39.7,-10.));
#10113=CARTESIAN_POINT('',(-141.,39.7,-10.));
#10114=CARTESIAN_POINT('',(-144.7,30.3,-10.));
#10115=CARTESIAN_POINT('',(-144.7,32.5,-10.));
#10116=CARTESIAN_POINT('',(-129.3,30.3,-10.));
#10117=CARTESIAN_POINT('',(-133.,30.3,-10.));
#10118=CARTESIAN_POINT('',(-129.3,2.5,-10.));
#10119=CARTESIAN_POINT('',(-143.262804086304,35.,-10.));
#10120=CARTESIAN_POINT('Origin',(-140.962804086304,35.,-10.));
#10121=CARTESIAN_POINT('Origin',(-133.037195913696,35.,-16.));
#10122=CARTESIAN_POINT('',(-135.037195913696,35.,-16.));
#10123=CARTESIAN_POINT('',(-135.037195913696,35.,-16.));
#10124=CARTESIAN_POINT('Origin',(-133.037195913696,35.,-16.));
#10125=CARTESIAN_POINT('Origin',(-140.962804086304,35.,-10.3));
#10126=CARTESIAN_POINT('',(-142.962804086304,35.,-10.3));
#10127=CARTESIAN_POINT('Origin',(-140.962804086304,35.,-10.3));
#10128=CARTESIAN_POINT('Origin',(-143.262804086304,35.,-10.3));
#10129=CARTESIAN_POINT('Origin',(-140.962804086304,35.,-16.));
#10130=CARTESIAN_POINT('',(-142.962804086304,35.,-16.));
#10131=CARTESIAN_POINT('',(-142.962804086304,35.,-16.));
#10132=CARTESIAN_POINT('Origin',(-140.962804086304,35.,-16.));
#10133=CARTESIAN_POINT('Origin',(-133.037195913696,-35.,-10.3));
#10134=CARTESIAN_POINT('',(-130.737195913696,-35.,-10.));
#10135=CARTESIAN_POINT('Origin',(-133.037195913696,-35.,-10.));
#10136=CARTESIAN_POINT('',(-131.037195913696,-35.,-10.3));
#10137=CARTESIAN_POINT('Origin',(-130.737195913696,-35.,-10.3));
#10138=CARTESIAN_POINT('',(-135.037195913696,-35.,-10.3));
#10139=CARTESIAN_POINT('Origin',(-133.037195913696,-35.,-10.3));
#10140=CARTESIAN_POINT('Origin',(-133.037195913696,-35.,-10.3));
#10141=CARTESIAN_POINT('Origin',(-137.,-35.,-10.));
#10142=CARTESIAN_POINT('',(-144.7,-30.3,-10.));
#10143=CARTESIAN_POINT('',(-129.3,-30.3,-10.));
#10144=CARTESIAN_POINT('',(-141.,-30.3,-10.));
#10145=CARTESIAN_POINT('',(-144.7,-39.7,-10.));
#10146=CARTESIAN_POINT('',(-144.7,-2.5,-10.));
#10147=CARTESIAN_POINT('',(-129.3,-39.7,-10.));
#10148=CARTESIAN_POINT('',(-141.,-39.7,-10.));
#10149=CARTESIAN_POINT('',(-129.3,-32.5,-10.));
#10150=CARTESIAN_POINT('',(-138.662804086304,-35.,-10.));
#10151=CARTESIAN_POINT('Origin',(-140.962804086304,-35.,-10.));
#10152=CARTESIAN_POINT('Origin',(-133.037195913696,-35.,-16.));
#10153=CARTESIAN_POINT('',(-135.037195913696,-35.,-16.));
#10154=CARTESIAN_POINT('',(-135.037195913696,-35.,-16.));
#10155=CARTESIAN_POINT('Origin',(-133.037195913696,-35.,-16.));
#10156=CARTESIAN_POINT('Origin',(-140.962804086304,-35.,-10.3));
#10157=CARTESIAN_POINT('',(-138.962804086304,-35.,-10.3));
#10158=CARTESIAN_POINT('Origin',(-138.662804086304,-35.,-10.3));
#10159=CARTESIAN_POINT('',(-142.962804086304,-35.,-10.3));
#10160=CARTESIAN_POINT('Origin',(-140.962804086304,-35.,-10.3));
#10161=CARTESIAN_POINT('Origin',(-140.962804086304,-35.,-10.3));
#10162=CARTESIAN_POINT('Origin',(-140.962804086304,-35.,-16.));
#10163=CARTESIAN_POINT('',(-142.962804086304,-35.,-16.));
#10164=CARTESIAN_POINT('',(-142.962804086304,-35.,-16.));
#10165=CARTESIAN_POINT('Origin',(-140.962804086304,-35.,-16.));
#10166=CARTESIAN_POINT('Origin',(-144.7,-39.7,-15.7));
#10167=CARTESIAN_POINT('',(-145.,-39.7,-15.7));
#10168=CARTESIAN_POINT('',(-144.7,-40.,-15.7));
#10169=CARTESIAN_POINT('Origin',(-144.7,-39.7,-15.7));
#10170=CARTESIAN_POINT('',(-144.7,-39.7,-16.));
#10171=CARTESIAN_POINT('Origin',(-144.7,-39.7,-15.7));
#10172=CARTESIAN_POINT('Origin',(-144.7,-39.7,-15.7));
#10173=CARTESIAN_POINT('Origin',(-129.3,-39.7,-15.7));
#10174=CARTESIAN_POINT('',(-129.3,-39.7,-16.));
#10175=CARTESIAN_POINT('',(-129.3,-40.,-15.7));
#10176=CARTESIAN_POINT('Origin',(-129.3,-39.7,-15.7));
#10177=CARTESIAN_POINT('',(-129.,-39.7,-15.7));
#10178=CARTESIAN_POINT('Origin',(-129.3,-39.7,-15.7));
#10179=CARTESIAN_POINT('Origin',(-129.3,-39.7,-15.7));
#10180=CARTESIAN_POINT('Origin',(-144.7,39.7,-15.7));
#10181=CARTESIAN_POINT('',(-144.7,39.7,-16.));
#10182=CARTESIAN_POINT('',(-144.7,40.,-15.7));
#10183=CARTESIAN_POINT('Origin',(-144.7,39.7,-15.7));
#10184=CARTESIAN_POINT('',(-145.,39.7,-15.7));
#10185=CARTESIAN_POINT('Origin',(-144.7,39.7,-15.7));
#10186=CARTESIAN_POINT('Origin',(-144.7,39.7,-15.7));
#10187=CARTESIAN_POINT('Origin',(-144.7,15.,-15.7));
#10188=CARTESIAN_POINT('',(-144.7,15.,-16.));
#10189=CARTESIAN_POINT('',(-145.,15.,-15.7));
#10190=CARTESIAN_POINT('Origin',(-144.7,-39.7,-10.3));
#10191=CARTESIAN_POINT('',(-145.,-39.7,-10.3));
#10192=CARTESIAN_POINT('Origin',(-144.7,-39.7,-10.3));
#10193=CARTESIAN_POINT('',(-144.7,-40.,-10.3));
#10194=CARTESIAN_POINT('Origin',(-144.7,-39.7,-10.3));
#10195=CARTESIAN_POINT('Origin',(-144.7,-39.7,-10.3));
#10196=CARTESIAN_POINT('Origin',(-144.7,-39.7,-8.));
#10197=CARTESIAN_POINT('',(-145.,-39.7,-8.));
#10198=CARTESIAN_POINT('',(-144.7,-40.,-8.));
#10199=CARTESIAN_POINT('Origin',(-129.3,39.7,-15.7));
#10200=CARTESIAN_POINT('',(-129.,39.7,-15.7));
#10201=CARTESIAN_POINT('',(-129.3,40.,-15.7));
#10202=CARTESIAN_POINT('Origin',(-129.3,39.7,-15.7));
#10203=CARTESIAN_POINT('',(-129.3,39.7,-16.));
#10204=CARTESIAN_POINT('Origin',(-129.3,39.7,-15.7));
#10205=CARTESIAN_POINT('Origin',(-129.3,39.7,-15.7));
#10206=CARTESIAN_POINT('Origin',(-129.3,-15.,-15.7));
#10207=CARTESIAN_POINT('',(-129.,-15.,-15.7));
#10208=CARTESIAN_POINT('',(-129.3,-15.,-16.));
#10209=CARTESIAN_POINT('Origin',(-141.,39.7,-15.7));
#10210=CARTESIAN_POINT('',(-141.,40.,-15.7));
#10211=CARTESIAN_POINT('',(-141.,39.7,-16.));
#10212=CARTESIAN_POINT('Origin',(-129.3,-39.7,-10.3));
#10213=CARTESIAN_POINT('',(-129.3,-40.,-10.3));
#10214=CARTESIAN_POINT('Origin',(-129.3,-39.7,-10.3));
#10215=CARTESIAN_POINT('',(-129.,-39.7,-10.3));
#10216=CARTESIAN_POINT('Origin',(-129.3,-39.7,-10.3));
#10217=CARTESIAN_POINT('Origin',(-129.3,-39.7,-10.3));
#10218=CARTESIAN_POINT('Origin',(-129.3,-39.7,-8.));
#10219=CARTESIAN_POINT('',(-129.3,-40.,-8.));
#10220=CARTESIAN_POINT('',(-129.,-39.7,-8.));
#10221=CARTESIAN_POINT('Origin',(-144.7,39.7,-10.3));
#10222=CARTESIAN_POINT('',(-145.,39.7,-10.3));
#10223=CARTESIAN_POINT('',(-144.7,40.,-10.3));
#10224=CARTESIAN_POINT('Origin',(-144.7,39.7,-10.3));
#10225=CARTESIAN_POINT('Origin',(-144.7,39.7,-10.3));
#10226=CARTESIAN_POINT('Origin',(-144.7,39.7,-10.3));
#10227=CARTESIAN_POINT('Origin',(-144.7,-30.3,-9.7));
#10228=CARTESIAN_POINT('',(-144.7,-30.,-9.7));
#10229=CARTESIAN_POINT('Origin',(-144.7,-30.3,-9.7));
#10230=CARTESIAN_POINT('',(-145.,-29.7,-9.7));
#10231=CARTESIAN_POINT('Origin',(-144.7,-29.7,-9.7));
#10232=CARTESIAN_POINT('',(-145.,-30.3,-10.3));
#10233=CARTESIAN_POINT('Origin',(-145.,-30.3,-9.7));
#10234=CARTESIAN_POINT('Origin',(-144.7,-30.3,-10.3));
#10235=CARTESIAN_POINT('Origin',(-129.3,39.7,-10.3));
#10236=CARTESIAN_POINT('',(-129.3,40.,-10.3));
#10237=CARTESIAN_POINT('',(-129.,39.7,-10.3));
#10238=CARTESIAN_POINT('Origin',(-129.3,39.7,-10.3));
#10239=CARTESIAN_POINT('Origin',(-129.3,39.7,-10.3));
#10240=CARTESIAN_POINT('Origin',(-129.3,39.7,-10.3));
#10241=CARTESIAN_POINT('Origin',(-141.,39.7,-10.3));
#10242=CARTESIAN_POINT('',(-141.,40.,-10.3));
#10243=CARTESIAN_POINT('Origin',(-129.3,-30.3,-9.7));
#10244=CARTESIAN_POINT('',(-129.,-30.3,-10.3));
#10245=CARTESIAN_POINT('',(-129.,-29.7,-9.7));
#10246=CARTESIAN_POINT('Origin',(-129.,-30.3,-9.7));
#10247=CARTESIAN_POINT('',(-129.3,-30.,-9.7));
#10248=CARTESIAN_POINT('Origin',(-129.3,-29.7,-9.7));
#10249=CARTESIAN_POINT('Origin',(-129.3,-30.3,-9.7));
#10250=CARTESIAN_POINT('Origin',(-129.3,-30.3,-10.3));
#10251=CARTESIAN_POINT('Origin',(-144.7,30.3,-9.7));
#10252=CARTESIAN_POINT('',(-145.,30.3,-10.3));
#10253=CARTESIAN_POINT('',(-145.,29.7,-9.7));
#10254=CARTESIAN_POINT('Origin',(-145.,30.3,-9.7));
#10255=CARTESIAN_POINT('',(-144.7,30.,-9.7));
#10256=CARTESIAN_POINT('Origin',(-144.7,29.7,-9.7));
#10257=CARTESIAN_POINT('Origin',(-144.7,30.3,-9.7));
#10258=CARTESIAN_POINT('Origin',(-144.7,30.3,-10.3));
#10259=CARTESIAN_POINT('Origin',(-144.7,-29.7,15.7));
#10260=CARTESIAN_POINT('',(-145.,-29.7,15.7));
#10261=CARTESIAN_POINT('',(-144.7,-29.7,16.));
#10262=CARTESIAN_POINT('Origin',(-144.7,-29.7,15.7));
#10263=CARTESIAN_POINT('',(-144.7,-30.,15.7));
#10264=CARTESIAN_POINT('Origin',(-144.7,-29.7,15.7));
#10265=CARTESIAN_POINT('Origin',(-144.7,-29.7,15.7));
#10266=CARTESIAN_POINT('Origin',(-144.7,-29.7,0.));
#10267=CARTESIAN_POINT('',(-144.7,-30.,0.));
#10268=CARTESIAN_POINT('',(-145.,-29.7,0.));
#10269=CARTESIAN_POINT('Origin',(-129.3,30.3,-9.7));
#10270=CARTESIAN_POINT('',(-129.3,30.,-9.7));
#10271=CARTESIAN_POINT('Origin',(-129.3,30.3,-9.7));
#10272=CARTESIAN_POINT('',(-129.,29.7,-9.7));
#10273=CARTESIAN_POINT('Origin',(-129.3,29.7,-9.7));
#10274=CARTESIAN_POINT('',(-129.,30.3,-10.3));
#10275=CARTESIAN_POINT('Origin',(-129.,30.3,-9.7));
#10276=CARTESIAN_POINT('Origin',(-129.3,30.3,-10.3));
#10277=CARTESIAN_POINT('Origin',(-129.3,-29.7,15.7));
#10278=CARTESIAN_POINT('',(-129.3,-30.,15.7));
#10279=CARTESIAN_POINT('',(-129.3,-29.7,16.));
#10280=CARTESIAN_POINT('Origin',(-129.3,-29.7,15.7));
#10281=CARTESIAN_POINT('',(-129.,-29.7,15.7));
#10282=CARTESIAN_POINT('Origin',(-129.3,-29.7,15.7));
#10283=CARTESIAN_POINT('Origin',(-129.3,-29.7,15.7));
#10284=CARTESIAN_POINT('Origin',(-129.3,-29.7,0.));
#10285=CARTESIAN_POINT('',(-129.3,-30.,0.));
#10286=CARTESIAN_POINT('',(-129.,-29.7,0.));
#10287=CARTESIAN_POINT('Origin',(-144.7,29.7,15.7));
#10288=CARTESIAN_POINT('',(-144.7,30.,15.7));
#10289=CARTESIAN_POINT('',(-144.7,29.7,16.));
#10290=CARTESIAN_POINT('Origin',(-144.7,29.7,15.7));
#10291=CARTESIAN_POINT('',(-145.,29.7,15.7));
#10292=CARTESIAN_POINT('Origin',(-144.7,29.7,15.7));
#10293=CARTESIAN_POINT('Origin',(-144.7,29.7,15.7));
#10294=CARTESIAN_POINT('Origin',(-144.7,29.7,0.));
#10295=CARTESIAN_POINT('',(-144.7,30.,0.));
#10296=CARTESIAN_POINT('',(-145.,29.7,0.));
#10297=CARTESIAN_POINT('Origin',(-144.7,-22.7999999999999,15.7));
#10298=CARTESIAN_POINT('',(-145.,-22.7999999999999,15.7));
#10299=CARTESIAN_POINT('',(-144.7,-22.4999999999999,15.7));
#10300=CARTESIAN_POINT('Origin',(-144.7,-22.7999999999999,15.7));
#10301=CARTESIAN_POINT('',(-144.7,-22.7999999999999,16.));
#10302=CARTESIAN_POINT('Origin',(-144.7,-22.7999999999999,15.7));
#10303=CARTESIAN_POINT('Origin',(-144.7,-22.7999999999999,15.7));
#10304=CARTESIAN_POINT('Origin',(-144.7,15.,15.7));
#10305=CARTESIAN_POINT('',(-144.7,15.,16.));
#10306=CARTESIAN_POINT('',(-145.,15.,15.7));
#10307=CARTESIAN_POINT('Origin',(-129.3,29.7,15.7));
#10308=CARTESIAN_POINT('',(-129.,29.7,15.7));
#10309=CARTESIAN_POINT('',(-129.3,29.7,16.));
#10310=CARTESIAN_POINT('Origin',(-129.3,29.7,15.7));
#10311=CARTESIAN_POINT('',(-129.3,30.,15.7));
#10312=CARTESIAN_POINT('Origin',(-129.3,29.7,15.7));
#10313=CARTESIAN_POINT('Origin',(-129.3,29.7,15.7));
#10314=CARTESIAN_POINT('Origin',(-129.3,29.7,0.));
#10315=CARTESIAN_POINT('',(-129.,29.7,0.));
#10316=CARTESIAN_POINT('',(-129.3,30.,0.));
#10317=CARTESIAN_POINT('Origin',(-133.,29.7,15.7));
#10318=CARTESIAN_POINT('',(-133.,29.7,16.));
#10319=CARTESIAN_POINT('',(-133.,30.,15.7));
#10320=CARTESIAN_POINT('Origin',(-129.3,-22.7999999999999,15.7));
#10321=CARTESIAN_POINT('',(-129.,-22.7999999999999,15.7));
#10322=CARTESIAN_POINT('',(-129.3,-22.7999999999999,16.));
#10323=CARTESIAN_POINT('Origin',(-129.3,-22.7999999999999,15.7));
#10324=CARTESIAN_POINT('',(-129.3,-22.4999999999999,15.7));
#10325=CARTESIAN_POINT('Origin',(-129.3,-22.7999999999999,15.7));
#10326=CARTESIAN_POINT('Origin',(-129.3,-22.7999999999999,15.7));
#10327=CARTESIAN_POINT('Origin',(-144.7,22.7999999999999,15.7));
#10328=CARTESIAN_POINT('',(-144.7,22.4999999999999,15.7));
#10329=CARTESIAN_POINT('',(-145.,22.7999999999999,15.7));
#10330=CARTESIAN_POINT('Origin',(-144.7,22.7999999999999,15.7));
#10331=CARTESIAN_POINT('',(-144.7,22.7999999999999,16.));
#10332=CARTESIAN_POINT('Origin',(-144.7,22.7999999999999,15.7));
#10333=CARTESIAN_POINT('Origin',(-144.7,22.7999999999999,15.7));
#10334=CARTESIAN_POINT('Origin',(-144.7,-22.7999999999999,8.));
#10335=CARTESIAN_POINT('',(-145.,-22.7999999999999,2.29525996204705));
#10336=CARTESIAN_POINT('',(-145.,-22.7999999999999,8.));
#10337=CARTESIAN_POINT('',(-144.7,-22.4999999999999,2.03896089378841));
#10338=CARTESIAN_POINT('',(-144.7,-22.4999999999999,8.));
#10339=CARTESIAN_POINT('Ctrl Pts',(-144.7,-22.4999999999999,2.03896089378841));
#10340=CARTESIAN_POINT('Ctrl Pts',(-144.729707021216,-22.4999999999999,
2.03896089378841));
#10341=CARTESIAN_POINT('Ctrl Pts',(-144.758777673282,-22.5044062942651,
2.04285168076791));
#10342=CARTESIAN_POINT('Ctrl Pts',(-144.817440852233,-22.5220432289933,
2.05836227087722));
#10343=CARTESIAN_POINT('Ctrl Pts',(-144.845615509175,-22.5359942380498,
2.07060652861162));
#10344=CARTESIAN_POINT('Ctrl Pts',(-144.902101216584,-22.5749600084548,
2.10457296342855));
#10345=CARTESIAN_POINT('Ctrl Pts',(-144.927927434013,-22.6017796731997,
2.12780612534896));
#10346=CARTESIAN_POINT('Ctrl Pts',(-144.964853191741,-22.6558870245156,
2.17419410934337));
#10347=CARTESIAN_POINT('Ctrl Pts',(-144.977648024164,-22.6827478353212,
2.19704892778962));
#10348=CARTESIAN_POINT('Ctrl Pts',(-144.995183002528,-22.7387435986925,
2.24427435404391));
#10349=CARTESIAN_POINT('Ctrl Pts',(-144.999750204092,-22.768135790235,2.26885093228759));
#10350=CARTESIAN_POINT('Ctrl Pts',(-144.999996676585,-22.7983695157586,
2.29390907943587));
#10351=CARTESIAN_POINT('Ctrl Pts',(-145.,-22.7991847191594,2.29458456964534));
#10352=CARTESIAN_POINT('Ctrl Pts',(-145.,-22.7999999999999,2.29525996204705));
#10353=CARTESIAN_POINT('Origin',(-129.3,22.7999999999999,15.7));
#10354=CARTESIAN_POINT('',(-129.,22.7999999999999,15.7));
#10355=CARTESIAN_POINT('',(-129.3,22.4999999999999,15.7));
#10356=CARTESIAN_POINT('Origin',(-129.3,22.7999999999999,15.7));
#10357=CARTESIAN_POINT('',(-129.3,22.7999999999999,16.));
#10358=CARTESIAN_POINT('Origin',(-129.3,22.7999999999999,15.7));
#10359=CARTESIAN_POINT('Origin',(-129.3,22.7999999999999,15.7));
#10360=CARTESIAN_POINT('Origin',(-129.3,-15.,15.7));
#10361=CARTESIAN_POINT('',(-129.3,-15.,16.));
#10362=CARTESIAN_POINT('',(-129.,-15.,15.7));
#10363=CARTESIAN_POINT('Origin',(-141.,22.7999999999999,15.7));
#10364=CARTESIAN_POINT('',(-141.,22.7999999999999,16.));
#10365=CARTESIAN_POINT('',(-141.,22.4999999999999,15.7));
#10366=CARTESIAN_POINT('Origin',(-129.3,-22.7999999999999,8.));
#10367=CARTESIAN_POINT('',(-129.3,-22.4999999999999,2.03896089378841));
#10368=CARTESIAN_POINT('',(-129.3,-22.4999999999999,8.));
#10369=CARTESIAN_POINT('',(-129.,-22.7999999999999,2.29525996204705));
#10370=CARTESIAN_POINT('',(-129.,-22.7999999999999,8.));
#10371=CARTESIAN_POINT('Ctrl Pts',(-129.,-22.7999999999999,2.29525996204705));
#10372=CARTESIAN_POINT('Ctrl Pts',(-129.,-22.7991847191433,2.29458456963201));
#10373=CARTESIAN_POINT('Ctrl Pts',(-129.000003323414,-22.798369515774,2.29390907945453));
#10374=CARTESIAN_POINT('Ctrl Pts',(-129.000249795909,-22.7681357900482,
2.26885093208373));
#10375=CARTESIAN_POINT('Ctrl Pts',(-129.004816997483,-22.7387435986578,
2.24427435401478));
#10376=CARTESIAN_POINT('Ctrl Pts',(-129.022351975836,-22.6827478353226,
2.19704892779083));
#10377=CARTESIAN_POINT('Ctrl Pts',(-129.035146808259,-22.6558870245162,
2.17419410934394));
#10378=CARTESIAN_POINT('Ctrl Pts',(-129.072072565987,-22.6017796731997,
2.12780612534895));
#10379=CARTESIAN_POINT('Ctrl Pts',(-129.097898783416,-22.5749600084547,
2.10457296342854));
#10380=CARTESIAN_POINT('Ctrl Pts',(-129.154384490824,-22.5359942380497,
2.07060652861162));
#10381=CARTESIAN_POINT('Ctrl Pts',(-129.182559147767,-22.5220432289933,
2.05836227087722));
#10382=CARTESIAN_POINT('Ctrl Pts',(-129.241222326718,-22.5044062942651,
2.04285168076791));
#10383=CARTESIAN_POINT('Ctrl Pts',(-129.270292978784,-22.4999999999999,
2.03896089378841));
#10384=CARTESIAN_POINT('Ctrl Pts',(-129.3,-22.4999999999999,2.03896089378841));
#10385=CARTESIAN_POINT('Origin',(-144.7,22.7999999999999,8.));
#10386=CARTESIAN_POINT('',(-144.7,22.4999999999999,2.03896089378841));
#10387=CARTESIAN_POINT('',(-144.7,22.4999999999999,8.));
#10388=CARTESIAN_POINT('',(-145.,22.7999999999999,2.29525996204705));
#10389=CARTESIAN_POINT('',(-145.,22.7999999999999,8.));
#10390=CARTESIAN_POINT('Ctrl Pts',(-145.,22.7999999999999,2.29525996204705));
#10391=CARTESIAN_POINT('Ctrl Pts',(-145.,22.7991847191433,2.29458456963199));
#10392=CARTESIAN_POINT('Ctrl Pts',(-144.999996676586,22.798369515774,2.29390907945454));
#10393=CARTESIAN_POINT('Ctrl Pts',(-144.99975020409,22.768135790048,2.26885093208354));
#10394=CARTESIAN_POINT('Ctrl Pts',(-144.995183002517,22.7387435986577,2.24427435401474));
#10395=CARTESIAN_POINT('Ctrl Pts',(-144.977648024164,22.6827478353226,2.19704892779082));
#10396=CARTESIAN_POINT('Ctrl Pts',(-144.964853191741,22.6558870245162,2.17419410934393));
#10397=CARTESIAN_POINT('Ctrl Pts',(-144.927927434013,22.6017796731997,2.12780612534896));
#10398=CARTESIAN_POINT('Ctrl Pts',(-144.902101216584,22.5749600084548,2.10457296342855));
#10399=CARTESIAN_POINT('Ctrl Pts',(-144.845615509175,22.5359942380498,2.07060652861164));
#10400=CARTESIAN_POINT('Ctrl Pts',(-144.817440852233,22.5220432289933,2.05836227087723));
#10401=CARTESIAN_POINT('Ctrl Pts',(-144.758777673282,22.5044062942651,2.04285168076791));
#10402=CARTESIAN_POINT('Ctrl Pts',(-144.729707021216,22.4999999999999,2.03896089378841));
#10403=CARTESIAN_POINT('Ctrl Pts',(-144.7,22.4999999999999,2.03896089378841));
#10404=CARTESIAN_POINT('Origin',(-129.3,22.7999999999999,8.));
#10405=CARTESIAN_POINT('',(-129.,22.7999999999999,2.29525996204705));
#10406=CARTESIAN_POINT('',(-129.,22.7999999999999,8.));
#10407=CARTESIAN_POINT('',(-129.3,22.4999999999999,2.03896089378841));
#10408=CARTESIAN_POINT('',(-129.3,22.4999999999999,8.));
#10409=CARTESIAN_POINT('Ctrl Pts',(-129.3,22.4999999999999,2.03896089378841));
#10410=CARTESIAN_POINT('Ctrl Pts',(-129.270292978784,22.4999999999999,2.03896089378841));
#10411=CARTESIAN_POINT('Ctrl Pts',(-129.241222326718,22.5044062942651,2.04285168076791));
#10412=CARTESIAN_POINT('Ctrl Pts',(-129.182559147767,22.5220432289932,2.05836227087722));
#10413=CARTESIAN_POINT('Ctrl Pts',(-129.154384490824,22.5359942380497,2.07060652861162));
#10414=CARTESIAN_POINT('Ctrl Pts',(-129.097898783416,22.5749600084547,2.10457296342855));
#10415=CARTESIAN_POINT('Ctrl Pts',(-129.072072565987,22.6017796731997,2.12780612534895));
#10416=CARTESIAN_POINT('Ctrl Pts',(-129.035146808259,22.6558870245162,2.17419410934394));
#10417=CARTESIAN_POINT('Ctrl Pts',(-129.022351975836,22.6827478353226,2.19704892779082));
#10418=CARTESIAN_POINT('Ctrl Pts',(-129.004816997483,22.7387435986577,2.24427435401479));
#10419=CARTESIAN_POINT('Ctrl Pts',(-129.000249795909,22.7681357900482,2.26885093208374));
#10420=CARTESIAN_POINT('Ctrl Pts',(-129.000003323414,22.798369515774,2.29390907945453));
#10421=CARTESIAN_POINT('Ctrl Pts',(-129.,22.7991847191433,2.29458456963201));
#10422=CARTESIAN_POINT('Ctrl Pts',(-129.,22.7999999999999,2.29525996204705));
#10423=CARTESIAN_POINT('Origin',(-144.7,-21.1999999999999,15.7));
#10424=CARTESIAN_POINT('',(-144.7,-21.4999999999999,15.7));
#10425=CARTESIAN_POINT('',(-145.,-21.1999999999999,15.7));
#10426=CARTESIAN_POINT('Origin',(-144.7,-21.1999999999999,15.7));
#10427=CARTESIAN_POINT('',(-144.7,-21.1999999999999,16.));
#10428=CARTESIAN_POINT('Origin',(-144.7,-21.1999999999999,15.7));
#10429=CARTESIAN_POINT('Origin',(-144.7,-21.1999999999999,15.7));
#10430=CARTESIAN_POINT('Origin',(-129.3,-21.1999999999999,15.7));
#10431=CARTESIAN_POINT('',(-129.,-21.1999999999999,15.7));
#10432=CARTESIAN_POINT('',(-129.3,-21.4999999999999,15.7));
#10433=CARTESIAN_POINT('Origin',(-129.3,-21.1999999999999,15.7));
#10434=CARTESIAN_POINT('',(-129.3,-21.1999999999999,16.));
#10435=CARTESIAN_POINT('Origin',(-129.3,-21.1999999999999,15.7));
#10436=CARTESIAN_POINT('Origin',(-129.3,-21.1999999999999,15.7));
#10437=CARTESIAN_POINT('Origin',(-144.7,21.1999999999999,15.7));
#10438=CARTESIAN_POINT('',(-145.,21.1999999999999,15.7));
#10439=CARTESIAN_POINT('',(-144.7,21.4999999999999,15.7));
#10440=CARTESIAN_POINT('Origin',(-144.7,21.1999999999999,15.7));
#10441=CARTESIAN_POINT('',(-144.7,21.1999999999999,16.));
#10442=CARTESIAN_POINT('Origin',(-144.7,21.1999999999999,15.7));
#10443=CARTESIAN_POINT('Origin',(-144.7,21.1999999999999,15.7));
#10444=CARTESIAN_POINT('Origin',(-144.7,15.,15.7));
#10445=CARTESIAN_POINT('',(-144.7,15.,16.));
#10446=CARTESIAN_POINT('',(-145.,15.,15.7));
#10447=CARTESIAN_POINT('Origin',(-129.3,21.1999999999999,15.7));
#10448=CARTESIAN_POINT('',(-129.,21.1999999999999,15.7));
#10449=CARTESIAN_POINT('',(-129.3,21.1999999999999,16.));
#10450=CARTESIAN_POINT('Origin',(-129.3,21.1999999999999,15.7));
#10451=CARTESIAN_POINT('',(-129.3,21.4999999999999,15.7));
#10452=CARTESIAN_POINT('Origin',(-129.3,21.1999999999999,15.7));
#10453=CARTESIAN_POINT('Origin',(-129.3,21.1999999999999,15.7));
#10454=CARTESIAN_POINT('Origin',(-129.3,21.1999999999999,1.01948044689421));
#10455=CARTESIAN_POINT('',(-129.3,21.4999999999999,2.03896089378841));
#10456=CARTESIAN_POINT('',(-129.3,21.4999999999999,1.01948044689421));
#10457=CARTESIAN_POINT('',(-129.,21.1999999999999,2.29525996204705));
#10458=CARTESIAN_POINT('',(-129.,21.1999999999999,1.01948044689421));
#10459=CARTESIAN_POINT('Ctrl Pts',(-129.,21.1999999999999,2.29525996204705));
#10460=CARTESIAN_POINT('Ctrl Pts',(-129.,21.2008152808565,2.29458456963201));
#10461=CARTESIAN_POINT('Ctrl Pts',(-129.000003323414,21.2016304842259,2.29390907945453));
#10462=CARTESIAN_POINT('Ctrl Pts',(-129.000249795909,21.2318642099517,2.26885093208371));
#10463=CARTESIAN_POINT('Ctrl Pts',(-129.004816997483,21.2612564013421,2.24427435401476));
#10464=CARTESIAN_POINT('Ctrl Pts',(-129.022351975836,21.3172521646773,2.19704892779083));
#10465=CARTESIAN_POINT('Ctrl Pts',(-129.035146808259,21.3441129754836,2.17419410934394));
#10466=CARTESIAN_POINT('Ctrl Pts',(-129.072072565987,21.3982203268002,2.12780612534896));
#10467=CARTESIAN_POINT('Ctrl Pts',(-129.097898783416,21.4250399915451,2.10457296342855));
#10468=CARTESIAN_POINT('Ctrl Pts',(-129.154384490824,21.4640057619501,2.07060652861162));
#10469=CARTESIAN_POINT('Ctrl Pts',(-129.182559147767,21.4779567710066,2.05836227087723));
#10470=CARTESIAN_POINT('Ctrl Pts',(-129.241222326718,21.4955937057348,2.04285168076791));
#10471=CARTESIAN_POINT('Ctrl Pts',(-129.270292978784,21.4999999999999,2.03896089378841));
#10472=CARTESIAN_POINT('Ctrl Pts',(-129.3,21.4999999999999,2.03896089378841));
#10473=CARTESIAN_POINT('Origin',(-141.,21.1999999999999,15.7));
#10474=CARTESIAN_POINT('',(-141.,21.1999999999999,16.));
#10475=CARTESIAN_POINT('',(-141.,21.4999999999999,15.7));
#10476=CARTESIAN_POINT('Origin',(-129.3,-15.,15.7));
#10477=CARTESIAN_POINT('',(-129.3,-15.,16.));
#10478=CARTESIAN_POINT('',(-129.,-15.,15.7));
#10479=CARTESIAN_POINT('Origin',(-144.7,21.1999999999999,1.01948044689421));
#10480=CARTESIAN_POINT('',(-145.,21.1999999999999,2.29525996204705));
#10481=CARTESIAN_POINT('',(-145.,21.1999999999999,1.01948044689421));
#10482=CARTESIAN_POINT('',(-144.7,21.4999999999999,2.03896089378841));
#10483=CARTESIAN_POINT('',(-144.7,21.4999999999999,1.01948044689421));
#10484=CARTESIAN_POINT('Ctrl Pts',(-144.7,21.4999999999999,2.03896089378841));
#10485=CARTESIAN_POINT('Ctrl Pts',(-144.729707021216,21.4999999999999,2.03896089378841));
#10486=CARTESIAN_POINT('Ctrl Pts',(-144.758777673282,21.4955937057347,2.04285168076792));
#10487=CARTESIAN_POINT('Ctrl Pts',(-144.817440852233,21.4779567710066,2.05836227087722));
#10488=CARTESIAN_POINT('Ctrl Pts',(-144.845615509175,21.4640057619501,2.07060652861162));
#10489=CARTESIAN_POINT('Ctrl Pts',(-144.902101216584,21.4250399915451,2.10457296342855));
#10490=CARTESIAN_POINT('Ctrl Pts',(-144.927927434013,21.3982203268002,2.12780612534895));
#10491=CARTESIAN_POINT('Ctrl Pts',(-144.964853191741,21.3441129754836,2.17419410934394));
#10492=CARTESIAN_POINT('Ctrl Pts',(-144.977648024164,21.3172521646773,2.19704892779082));
#10493=CARTESIAN_POINT('Ctrl Pts',(-144.995183002517,21.2612564013421,2.24427435401479));
#10494=CARTESIAN_POINT('Ctrl Pts',(-144.99975020409,21.2318642099517,2.26885093208373));
#10495=CARTESIAN_POINT('Ctrl Pts',(-144.999996676586,21.2016304842259,2.29390907945453));
#10496=CARTESIAN_POINT('Ctrl Pts',(-145.,21.2008152808565,2.29458456963201));
#10497=CARTESIAN_POINT('Ctrl Pts',(-145.,21.1999999999999,2.29525996204705));
#10498=CARTESIAN_POINT('Origin',(-141.,-21.1999999999999,15.7));
#10499=CARTESIAN_POINT('',(-141.,-21.1999999999999,16.));
#10500=CARTESIAN_POINT('',(-141.,-21.4999999999999,15.7));
#10501=CARTESIAN_POINT('Origin',(-129.3,-21.1999999999999,1.01948044689421));
#10502=CARTESIAN_POINT('',(-129.,-21.1999999999999,2.29525996204705));
#10503=CARTESIAN_POINT('',(-129.,-21.1999999999999,1.01948044689421));
#10504=CARTESIAN_POINT('',(-129.3,-21.4999999999999,2.03896089378841));
#10505=CARTESIAN_POINT('',(-129.3,-21.4999999999999,1.01948044689421));
#10506=CARTESIAN_POINT('Ctrl Pts',(-129.3,-21.4999999999999,2.03896089378841));
#10507=CARTESIAN_POINT('Ctrl Pts',(-129.270292978784,-21.4999999999999,
2.03896089378841));
#10508=CARTESIAN_POINT('Ctrl Pts',(-129.241222326718,-21.4955937057347,
2.04285168076791));
#10509=CARTESIAN_POINT('Ctrl Pts',(-129.182559147767,-21.4779567710066,
2.05836227087723));
#10510=CARTESIAN_POINT('Ctrl Pts',(-129.154384490824,-21.4640057619501,
2.07060652861162));
#10511=CARTESIAN_POINT('Ctrl Pts',(-129.097898783416,-21.4250399915451,
2.10457296342855));
#10512=CARTESIAN_POINT('Ctrl Pts',(-129.072072565987,-21.3982203268002,
2.12780612534895));
#10513=CARTESIAN_POINT('Ctrl Pts',(-129.035146808259,-21.3441129754836,
2.17419410934393));
#10514=CARTESIAN_POINT('Ctrl Pts',(-129.022351975836,-21.3172521646773,
2.19704892779082));
#10515=CARTESIAN_POINT('Ctrl Pts',(-129.004816997483,-21.2612564013421,
2.24427435401479));
#10516=CARTESIAN_POINT('Ctrl Pts',(-129.000249795909,-21.2318642099517,
2.26885093208373));
#10517=CARTESIAN_POINT('Ctrl Pts',(-129.000003323414,-21.2016304842259,
2.29390907945453));
#10518=CARTESIAN_POINT('Ctrl Pts',(-129.,-21.2008152808565,2.29458456963201));
#10519=CARTESIAN_POINT('Ctrl Pts',(-129.,-21.1999999999999,2.29525996204705));
#10520=CARTESIAN_POINT('Origin',(-129.3,21.9999999999999,-1.92966607280848));
#10521=CARTESIAN_POINT('Origin',(-129.3,21.9999999999999,-1.92966607280848));
#10522=CARTESIAN_POINT('Origin',(-129.,21.9999999999999,-1.92966607280848));
#10523=CARTESIAN_POINT('Origin',(-144.7,-21.1999999999999,1.01948044689421));
#10524=CARTESIAN_POINT('',(-144.7,-21.4999999999999,2.03896089378841));
#10525=CARTESIAN_POINT('',(-144.7,-21.4999999999999,1.01948044689421));
#10526=CARTESIAN_POINT('',(-145.,-21.1999999999999,2.29525996204705));
#10527=CARTESIAN_POINT('',(-145.,-21.1999999999999,1.01948044689421));
#10528=CARTESIAN_POINT('Ctrl Pts',(-145.,-21.1999999999999,2.29525996204705));
#10529=CARTESIAN_POINT('Ctrl Pts',(-145.,-21.2008152808404,2.29458456964534));
#10530=CARTESIAN_POINT('Ctrl Pts',(-144.999996676585,-21.2016304842412,
2.29390907943587));
#10531=CARTESIAN_POINT('Ctrl Pts',(-144.999750204092,-21.2318642097648,
2.26885093228761));
#10532=CARTESIAN_POINT('Ctrl Pts',(-144.995183002528,-21.2612564013074,
2.24427435404393));
#10533=CARTESIAN_POINT('Ctrl Pts',(-144.977648024164,-21.3172521646786,
2.19704892778962));
#10534=CARTESIAN_POINT('Ctrl Pts',(-144.964853191741,-21.3441129754842,
2.17419410934337));
#10535=CARTESIAN_POINT('Ctrl Pts',(-144.927927434013,-21.3982203268002,
2.12780612534895));
#10536=CARTESIAN_POINT('Ctrl Pts',(-144.902101216584,-21.4250399915451,
2.10457296342854));
#10537=CARTESIAN_POINT('Ctrl Pts',(-144.845615509175,-21.4640057619501,
2.07060652861161));
#10538=CARTESIAN_POINT('Ctrl Pts',(-144.817440852233,-21.4779567710066,
2.05836227087722));
#10539=CARTESIAN_POINT('Ctrl Pts',(-144.758777673282,-21.4955937057347,
2.04285168076792));
#10540=CARTESIAN_POINT('Ctrl Pts',(-144.729707021216,-21.4999999999999,
2.03896089378841));
#10541=CARTESIAN_POINT('Ctrl Pts',(-144.7,-21.4999999999999,2.03896089378841));
#10542=CARTESIAN_POINT('Origin',(-144.7,21.9999999999999,-1.92966607280848));
#10543=CARTESIAN_POINT('Origin',(-145.,21.9999999999999,-1.92966607280848));
#10544=CARTESIAN_POINT('Origin',(-144.7,21.9999999999999,-1.92966607280848));
#10545=CARTESIAN_POINT('Origin',(-129.3,-21.9999999999999,-1.92966607280848));
#10546=CARTESIAN_POINT('Origin',(-129.,-21.9999999999999,-1.92966607280848));
#10547=CARTESIAN_POINT('Origin',(-129.3,-21.9999999999999,-1.92966607280848));
#10548=CARTESIAN_POINT('Origin',(-144.7,-21.9999999999999,-1.92966607280848));
#10549=CARTESIAN_POINT('Origin',(-144.7,-21.9999999999999,-1.92966607280848));
#10550=CARTESIAN_POINT('Origin',(-145.,-21.9999999999999,-1.92966607280848));
#10551=CARTESIAN_POINT('Origin',(-144.7,15.,15.7));
#10552=CARTESIAN_POINT('',(-144.7,15.,16.));
#10553=CARTESIAN_POINT('',(-145.,15.,15.7));
#10554=CARTESIAN_POINT('Origin',(-141.,-22.7999999999999,15.7));
#10555=CARTESIAN_POINT('',(-141.,-22.7999999999999,16.));
#10556=CARTESIAN_POINT('',(-141.,-22.4999999999999,15.7));
#10557=CARTESIAN_POINT('Origin',(-129.3,-15.,15.7));
#10558=CARTESIAN_POINT('',(-129.3,-15.,16.));
#10559=CARTESIAN_POINT('',(-129.,-15.,15.7));
#10560=CARTESIAN_POINT('Origin',(-141.,-29.7,15.7));
#10561=CARTESIAN_POINT('',(-141.,-29.7,16.));
#10562=CARTESIAN_POINT('',(-141.,-30.,15.7));
#10563=CARTESIAN_POINT('Origin',(-129.3,2.5,-10.3));
#10564=CARTESIAN_POINT('',(-129.,2.5,-10.3));
#10565=CARTESIAN_POINT('Origin',(-133.,30.3,-9.7));
#10566=CARTESIAN_POINT('',(-133.,30.,-9.7));
#10567=CARTESIAN_POINT('Origin',(-144.7,32.5,-10.3));
#10568=CARTESIAN_POINT('',(-145.,32.5,-10.3));
#10569=CARTESIAN_POINT('Origin',(-141.,-30.3,-9.7));
#10570=CARTESIAN_POINT('',(-141.,-30.,-9.7));
#10571=CARTESIAN_POINT('Origin',(-129.3,-32.5,-10.3));
#10572=CARTESIAN_POINT('',(-129.,-32.5,-10.3));
#10573=CARTESIAN_POINT('Origin',(-129.3,39.7,-8.));
#10574=CARTESIAN_POINT('',(-129.,39.7,-8.));
#10575=CARTESIAN_POINT('',(-129.3,40.,-8.));
#10576=CARTESIAN_POINT('Origin',(-144.7,-2.5,-10.3));
#10577=CARTESIAN_POINT('',(-145.,-2.5,-10.3));
#10578=CARTESIAN_POINT('Origin',(-144.7,39.7,-8.));
#10579=CARTESIAN_POINT('',(-144.7,40.,-8.));
#10580=CARTESIAN_POINT('',(-145.,39.7,-8.));
#10581=CARTESIAN_POINT('Origin',(-141.,-39.7,-10.3));
#10582=CARTESIAN_POINT('',(-141.,-40.,-10.3));
#10583=CARTESIAN_POINT('Origin',(-141.,-39.7,-15.7));
#10584=CARTESIAN_POINT('',(-141.,-39.7,-16.));
#10585=CARTESIAN_POINT('',(-141.,-40.,-15.7));
#10586=CARTESIAN_POINT('Origin',(-145.,21.4999999999999,2.03896089378841));
#10587=CARTESIAN_POINT('',(-145.,21.4999999999999,2.03896089378841));
#10588=CARTESIAN_POINT('Origin',(-145.,21.9999999999999,-1.92966607280848));
#10589=CARTESIAN_POINT('',(-145.,22.4999999999999,2.03896089378841));
#10590=CARTESIAN_POINT('Origin',(-145.,-21.9999999999999,-1.92966607280848));
#10591=CARTESIAN_POINT('',(-145.,-21.4999999999999,2.03896089378841));
#10592=CARTESIAN_POINT('',(-145.,-22.4999999999999,2.03896089378841));
#10593=CARTESIAN_POINT('Origin',(-145.,-21.4999999999999,2.03896089378841));
#10594=CARTESIAN_POINT('Origin',(-137.,-4.44089209850063E-15,-16.));
#10595=CARTESIAN_POINT('Origin',(-145.,-40.,-16.));
#10596=CARTESIAN_POINT('Origin',(-145.,40.,-16.));
#10597=CARTESIAN_POINT('Origin',(-145.,-30.,0.));
#10598=CARTESIAN_POINT('Origin',(-137.,-4.44089209850063E-15,16.));
#10599=CARTESIAN_POINT('Origin',(-129.,30.,0.));
#10600=CARTESIAN_POINT('Origin',(-137.,-4.44089209850063E-15,16.));
#10601=CARTESIAN_POINT('Origin',(-145.,30.,0.));
#10602=CARTESIAN_POINT('Origin',(-137.,-4.44089209850063E-15,16.));
#10603=CARTESIAN_POINT('Origin',(-129.,-30.,0.));
#10604=CARTESIAN_POINT('Origin',(-145.,22.4999999999999,16.));
#10605=CARTESIAN_POINT('Origin',(-145.,-22.4999999999999,16.));
#10626=UNCERTAINTY_MEASURE_WITH_UNIT(LENGTH_MEASURE(0.01),#10640,
'DISTANCE_ACCURACY_VALUE',
'Maximum model space distance between geometric entities at asserted c
onnectivities');
#10627=UNCERTAINTY_MEASURE_WITH_UNIT(LENGTH_MEASURE(0.01),#10640,
'DISTANCE_ACCURACY_VALUE',
'Maximum model space distance between geometric entities at asserted c
onnectivities');
#10638=(
GEOMETRIC_REPRESENTATION_CONTEXT(3)
GLOBAL_UNCERTAINTY_ASSIGNED_CONTEXT((#10626))
GLOBAL_UNIT_ASSIGNED_CONTEXT((#10640,#10642,#10643))
REPRESENTATION_CONTEXT('','3D')
);
#10639=(
GEOMETRIC_REPRESENTATION_CONTEXT(3)
GLOBAL_UNCERTAINTY_ASSIGNED_CONTEXT((#10627))
GLOBAL_UNIT_ASSIGNED_CONTEXT((#10640,#10642,#10643))
REPRESENTATION_CONTEXT('','3D')
);
#10640=(
LENGTH_UNIT()
NAMED_UNIT(*)
SI_UNIT(.MILLI.,.METRE.)
);
#10642=(
NAMED_UNIT(*)
PLANE_ANGLE_UNIT()
SI_UNIT($,.RADIAN.)
);
#10643=(
NAMED_UNIT(*)
SI_UNIT($,.STERADIAN.)
SOLID_ANGLE_UNIT()
);
#10654=SHAPE_DEFINITION_REPRESENTATION(#10665,#10686);
#10665=PRODUCT_DEFINITION_SHAPE('',$,#10698);
#10686=SHAPE_REPRESENTATION('',(#6489),#10638);
#10687=PRODUCT_DEFINITION_CONTEXT('part definition',#10722,'design');
#10698=PRODUCT_DEFINITION('Front_Block','Front_Block',#10709,#10687);
#10709=PRODUCT_DEFINITION_FORMATION('',$,#10734);
#10722=APPLICATION_CONTEXT(
'Core Data for Automotive Mechanical Design Process');
#10723=PRODUCT_CONTEXT('part definition',#10722,'mechanical');
#10734=PRODUCT('Front_Block','Front_Block',$,(#10723));
#10763=COLOUR_RGB('Dark Blue',0.08,0.2,0.34);
#10764=FILL_AREA_STYLE_COLOUR('',#10763);
#10765=FILL_AREA_STYLE('',(#10764));
#10766=SURFACE_STYLE_FILL_AREA(#10765);
#10767=SURFACE_SIDE_STYLE('',(#10766));
#10768=SURFACE_STYLE_USAGE(.BOTH.,#10767);
#10769=PRESENTATION_STYLE_ASSIGNMENT((#10768));
ENDSEC;
END-ISO-10303-21;
